ISO-10303-21;
HEADER;
FILE_DESCRIPTION (('STEP AP214'),
    '1' );
FILE_NAME ('Part2.step',
    '2026-11-01T05:08:46',
    ( '' ),
    ( '' ),
    'SwSTEP 2.0',
    'SolidWorks 2024',
    '' );
FILE_SCHEMA (( 'AUTOMOTIVE_DESIGN' ));
ENDSEC;

DATA;
#26=CARTESIAN_POINT ( 'NONE',  ( 56.72999999999999687, 290.3130897954761735, 29.03130897954726564 ) ) ;
#53=B_SPLINE_CURVE_WITH_KNOTS ( 'NONE', 3,
 ( #5779, #7371, #12713, #3697, #6084, #4964, #16576, #10218, #14084, #11332 ),
 .UNSPECIFIED., .F., .F.,
 ( 4, 2, 2, 2, 4 ),
 ( 0.000000000000000000, 0.2500000000000000000, 0.5000000000000000000, 0.7500000000000000000, 1.000000000000000000 ),
 .UNSPECIFIED. ) ;
#64=DIRECTION ( 'NONE',  ( 0.000000000000000000, 1.000000000000000000, -2.081668171172169746E-16 ) ) ;
#86=CARTESIAN_POINT ( 'NONE',  ( 0.5437585709472483320, 286.2028147183448823, 37.27096646979387629 ) ) ;
#100=DIRECTION ( 'NONE',  ( 3.491481338843133355E-15, -0.9950371902099891530, -0.09950371902099770793 ) ) ;
#107=AXIS2_PLACEMENT_3D ( 'NONE', #13523, #4147, #12231 ) ;
#109=AXIS2_PLACEMENT_3D ( 'NONE', #15496, #14284, #3731 ) ;
#135=SHAPE_REPRESENTATION ( 'Part2', ( #1488 ), #2021 ) ;
#222=STYLED_ITEM ( 'NONE', ( #8319 ), #8493 ) ;
#242=CARTESIAN_POINT ( 'NONE',  ( -3.302699999999637814, 285.9661841259148787, 37.54929111636468519 ) ) ;
#289=EDGE_CURVE ( 'NONE', #6952, #11437, #8821, .T. ) ;
#326=CARTESIAN_POINT ( 'NONE',  ( -2.493494276500600293, 287.9232781991976822, 37.61078711647744655 ) ) ;
#348=CARTESIAN_POINT ( 'NONE',  ( 0.000000000000000000, 239.4632308570078294, 71.73739990498292229 ) ) ;
#349=LINE ( 'NONE', #7808, #15445 ) ;
#390=EDGE_LOOP ( 'NONE', ( #8951, #12399, #14198, #7983 ) ) ;
#393=DIRECTION ( 'NONE',  ( -0.000000000000000000, 0.09950371902100807464, -0.9950371902099882648 ) ) ;
#418=DIRECTION ( 'NONE',  ( -1.000000000000000000, -0.000000000000000000, -0.000000000000000000 ) ) ;
#439=DIRECTION ( 'NONE',  ( 0.000000000000000000, 0.000000000000000000, 1.000000000000000000 ) ) ;
#462=CYLINDRICAL_SURFACE ( 'NONE', #9166, 4.006599999998678108 ) ;
#466=CARTESIAN_POINT ( 'NONE',  ( 0.7365999999999761627, 286.2094592450220034, 37.20452120302223875 ) ) ;
#473=VECTOR ( 'NONE', #673, 1000.000000000000000 ) ;
#489=CARTESIAN_POINT ( 'NONE',  ( -3.165718926336560823, 192.4396550164971984, 37.56780454546862558 ) ) ;
#541=ORIENTED_EDGE ( 'NONE', *, *, #2434, .F. ) ;
#574=DIRECTION ( 'NONE',  ( -1.000000000000000000, 3.474153781073081543E-15, -3.474153781073103631E-16 ) ) ;
#619=AXIS2_PLACEMENT_3D ( 'NONE', #348, #16146, #439 ) ;
#626=ORIENTED_EDGE ( 'NONE', *, *, #1932, .T. ) ;
#661=VECTOR ( 'NONE', #10165, 1000.000000000000114 ) ;
#673=DIRECTION ( 'NONE',  ( -1.000000000000000000, 1.798225651005137147E-12, 1.798225651005303603E-13 ) ) ;
#677=CARTESIAN_POINT ( 'NONE',  ( -1.725642888248450024, 190.2785135797052192, 37.61614439054952186 ) ) ;
#710=( NAMED_UNIT ( * ) PLANE_ANGLE_UNIT ( ) SI_UNIT ( $, .RADIAN. ) );
#712=EDGE_LOOP ( 'NONE', ( #7284, #9599, #2475, #11333 ) ) ;
#726=ORIENTED_EDGE ( 'NONE', *, *, #15567, .T. ) ;
#798=VECTOR ( 'NONE', #16726, 1000.000000000000000 ) ;
#814=FACE_OUTER_BOUND ( 'NONE', #2669, .T. ) ;
#832=CIRCLE ( 'NONE', #3026, 0.7365999999986965197 ) ;
#844=CARTESIAN_POINT ( 'NONE',  ( 7.230770027832480594E-13, 214.4632308570090800, 287.5298983642209123 ) ) ;
#854=FACE_OUTER_BOUND ( 'NONE', #5998, .T. ) ;
#874=CARTESIAN_POINT ( 'NONE',  ( -3.270000000000000462, 220.0768326692952996, 286.9685381829922903 ) ) ;
#877=LINE ( 'NONE', #9899, #2074 ) ;
#916=ORIENTED_EDGE ( 'NONE', *, *, #6292, .T. ) ;
#925=CARTESIAN_POINT ( 'NONE',  ( 0.7365999999999708336, 189.4306931408914920, 37.53315213583260856 ) ) ;
#977=AXIS2_PLACEMENT_3D ( 'NONE', #10796, #8211, #64 ) ;
#997=VERTEX_POINT ( 'NONE', #8272 ) ;
#1058=CARTESIAN_POINT ( 'NONE',  ( -3.269999999998713491, 260.4765148507196386, 287.1312267635918829 ) ) ;
#1076=CARTESIAN_POINT ( 'NONE',  ( 0.7366000000000088033, 192.7170024689980323, 37.20452120302199006 ) ) ;
#1102=EDGE_CURVE ( 'NONE', #14019, #15661, #53, .T. ) ;
#1108=EDGE_CURVE ( 'NONE', #11237, #10016, #3215, .T. ) ;
#1118=ORIENTED_EDGE ( 'NONE', *, *, #1108, .F. ) ;
#1153=ORIENTED_EDGE ( 'NONE', *, *, #1515, .F. ) ;
#1169=CARTESIAN_POINT ( 'NONE',  ( 0.05133912195990903565, 193.2999246972671870, 37.48177757739162530 ) ) ;
#1173=CARTESIAN_POINT ( 'NONE',  ( 1.286622718088565479E-12, 285.4366476906530465, 37.52989836422118941 ) ) ;
#1179=VECTOR ( 'NONE', #7670, 1000.000000000000114 ) ;
#1183=EDGE_CURVE ( 'NONE', #8690, #14834, #11730, .T. ) ;
#1197=CIRCLE ( 'NONE', #10802, 15.00000000000000000 ) ;
#1219=PLANE ( 'NONE',  #16820 ) ;
#1265=VECTOR ( 'NONE', #8841, 1000.000000000000227 ) ;
#1307=LINE ( 'NONE', #26, #15133 ) ;
#1354=ADVANCED_FACE ( 'NONE', ( #3083, #8061 ), #15955, .F. ) ;
#1418=VERTEX_POINT ( 'NONE', #6382 ) ;
#1433=CARTESIAN_POINT ( 'NONE',  ( -3.302699999998713665, 285.4366476906446337, 37.52989836422034386 ) ) ;
#1488=AXIS2_PLACEMENT_3D ( 'NONE', #3280, #8693, #15217 ) ;
#1495=FACE_OUTER_BOUND ( 'NONE', #10710, .T. ) ;
#1511=VERTEX_POINT ( 'NONE', #10436 ) ;
#1515=EDGE_CURVE ( 'NONE', #12302, #1865, #3914, .T. ) ;
#1519=VECTOR ( 'NONE', #4527, 1000.000000000000114 ) ;
#1553=LINE ( 'NONE', #14601, #2317 ) ;
#1592=EDGE_LOOP ( 'NONE', ( #3233, #16653, #12543, #5964 ) ) ;
#1603=AXIS2_PLACEMENT_3D ( 'NONE', #15323, #6274, #8796 ) ;
#1610=LINE ( 'NONE', #4441, #12374 ) ;
#1626=DIRECTION ( 'NONE',  ( -1.000000000000000000, -0.000000000000000000, 0.000000000000000000 ) ) ;
#1630=CARTESIAN_POINT ( 'NONE',  ( 1.250085104875786612E-12, 218.4499468633019603, 287.1312267635915987 ) ) ;
#1636=EDGE_LOOP ( 'NONE', ( #9639, #14899, #7557, #14166 ) ) ;
#1637=CARTESIAN_POINT ( 'NONE',  ( -2.736197741142289506E-16, 217.7170024689957586, 287.2045212030222388 ) ) ;
#1670=VECTOR ( 'NONE', #12977, 1000.000000000000000 ) ;
#1693=VERTEX_POINT ( 'NONE', #12655 ) ;
#1702=VECTOR ( 'NONE', #11528, 1000.000000000000000 ) ;
#1713=VECTOR ( 'NONE', #16909, 1000.000000000000000 ) ;
#1738=ADVANCED_FACE ( 'NONE', ( #16680 ), #4747, .T. ) ;
#1776=CARTESIAN_POINT ( 'NONE',  ( -0.3121190734724890725, 189.5736389302157647, 37.58596727633949541 ) ) ;
#1781=DIRECTION ( 'NONE',  ( 0.000000000000000000, -0.09950371902100227373, -0.9950371902099888199 ) ) ;
#1787=CARTESIAN_POINT ( 'NONE',  ( 1.116005356545072604E-12, 285.5359281317236650, 37.50626614651405788 ) ) ;
#1832=CARTESIAN_POINT ( 'NONE',  ( 0.000000000000000000, 258.8496290447203592, 286.9685381829918924 ) ) ;
#1865=VERTEX_POINT ( 'NONE', #7896 ) ;
#1877=DIRECTION ( 'NONE',  ( -1.000000000000000000, 3.424802208873653704E-15, 9.473616975916768164E-35 ) ) ;
#1899=VERTEX_POINT ( 'NONE', #14521 ) ;
#1922=CARTESIAN_POINT ( 'NONE',  ( 56.72999999999999687, 189.4632308570086536, 37.52989836422092651 ) ) ;
#1927=DIRECTION ( 'NONE',  ( 0.000000000000000000, -1.000000000000000000, 2.220446049250308742E-15 ) ) ;
#1932=EDGE_CURVE ( 'NONE', #14417, #11237, #9548, .T. ) ;
#1950=CARTESIAN_POINT ( 'NONE',  ( 0.2839248860676515940, 192.8804468505487932, 37.35595106346518435 ) ) ;
#1968=ORIENTED_EDGE ( 'NONE', *, *, #6535, .F. ) ;
#1989=DIRECTION ( 'NONE',  ( -1.000000000000000000, -1.622872818267927724E-12, 1.623597793334635938E-13 ) ) ;
#2021=( GEOMETRIC_REPRESENTATION_CONTEXT ( 3 ) GLOBAL_UNCERTAINTY_ASSIGNED_CONTEXT ( ( #12027 ) ) GLOBAL_UNIT_ASSIGNED_CONTEXT ( ( #12468, #710, #9979 ) ) REPRESENTATION_CONTEXT ( 'NONE', 'WORKASPACE' ) );
#2074=VECTOR ( 'NONE', #6098, 1000.000000000000227 ) ;
#2090=EDGE_CURVE ( 'NONE', #14834, #15661, #2391, .T. ) ;
#2117=CARTESIAN_POINT ( 'NONE',  ( 1.391674230819584651E-12, 193.3905335822941538, 37.50626614651405788 ) ) ;
#2122=ORIENTED_EDGE ( 'NONE', *, *, #15669, .T. ) ;
#2124=EDGE_CURVE ( 'NONE', #15922, #4232, #4803, .T. ) ;
#2204=CARTESIAN_POINT ( 'NONE',  ( -1.141714397801704670E-14, 289.4632308570086252, 37.52989836422091230 ) ) ;
#2206=ORIENTED_EDGE ( 'NONE', *, *, #6634, .T. ) ;
#2244=ORIENTED_EDGE ( 'NONE', *, *, #9228, .T. ) ;
#2289=CIRCLE ( 'NONE', #107, 15.00000000000000000 ) ;
#2296=AXIS2_PLACEMENT_3D ( 'NONE', #4671, #8207, #1781 ) ;
#2317=VECTOR ( 'NONE', #5404, 1000.000000000000000 ) ;
#2319=AXIS2_PLACEMENT_3D ( 'NONE', #7354, #16390, #5740 ) ;
#2326=LINE ( 'NONE', #11183, #11674 ) ;
#2378=DIRECTION ( 'NONE',  ( 4.930380657631322689E-32, 0.09950371902099953980, 0.9950371902099890420 ) ) ;
#2391=LINE ( 'NONE', #7536, #14228 ) ;
#2393=ORIENTED_EDGE ( 'NONE', *, *, #16215, .F. ) ;
#2410=CARTESIAN_POINT ( 'NONE',  ( 0.7366000000000293424, 218.4499468633031825, 287.1312267635914850 ) ) ;
#2428=EDGE_LOOP ( 'NONE', ( #9790, #15179, #726, #9313 ) ) ;
#2432=LINE ( 'NONE', #5010, #10989 ) ;
#2434=EDGE_CURVE ( 'NONE', #1511, #2958, #5881, .T. ) ;
#2436=ORIENTED_EDGE ( 'NONE', *, *, #4789, .F. ) ;
#2455=EDGE_CURVE ( 'NONE', #1693, #3926, #7491, .T. ) ;
#2474=CARTESIAN_POINT ( 'NONE',  ( 0.07938566280166349520, 285.8325239394490609, 37.43526655022222371 ) ) ;
#2475=ORIENTED_EDGE ( 'NONE', *, *, #1932, .F. ) ;
#2503=CARTESIAN_POINT ( 'NONE',  ( -3.270000000000000462, 258.7934930265974458, 287.5298983642207986 ) ) ;
#2504=LINE ( 'NONE', #1058, #661 ) ;
#2597=B_SPLINE_SURFACE_WITH_KNOTS ( 'NONE', 1, 3, ( 
 ( #925, #12432, #7097, #3419, #16632, #9699, #15016, #13650, #4690, #8410 ),
 ( #8743, #9947, #8488, #7427, #677, #12350, #13893, #13729, #13976, #6148 ),
 ( #14935, #3174, #9786, #16384, #1950, #5905, #6060, #4614, #2117, #7348 ),
 ( #9862, #8914, #6386, #4865, #15599, #6225, #12777, #1169, #3919, #10288 ) ),
 .UNSPECIFIED., .F., .F., .F.,
 ( 2, 1, 1, 2 ),
 ( 4, 2, 2, 2, 4 ),
 ( -0.01000000000000000021, 0.000000000000000000, 1.000000000000000000, 1.010099999999999998 ),
 ( 0.000000000000000000, 0.2500000000000000000, 0.5000000000000000000, 0.7500000000000000000, 1.000000000000000000 ),
 .UNSPECIFIED. ) ;
#2629=DIRECTION ( 'NONE',  ( -1.000000000000000000, -2.911324084205185756E-15, -2.422066625794664503E-16 ) ) ;
#2632=ORIENTED_EDGE ( 'NONE', *, *, #289, .F. ) ;
#2642=DIRECTION ( 'NONE',  ( 3.407805566942604354E-15, 0.9950371902099891530, -0.09950371902099955368 ) ) ;
#2667=EDGE_CURVE ( 'NONE', #1418, #15054, #8367, .T. ) ;
#2669=EDGE_LOOP ( 'NONE', ( #6409, #15053, #13431, #10159 ) ) ;
#2683=COLOUR_RGB ( '', 0.40784314, 0.44705882, 0.49803922) ;
#2684=ORIENTED_EDGE ( 'NONE', *, *, #6535, .T. ) ;
#2719=CARTESIAN_POINT ( 'NONE',  ( 0.3822672831237738378, 286.0749473089381922, 37.32528944829249440 ) ) ;
#2747=ORIENTED_EDGE ( 'NONE', *, *, #2763, .T. ) ;
#2758=ORIENTED_EDGE ( 'NONE', *, *, #12966, .T. ) ;
#2763=EDGE_CURVE ( 'NONE', #9809, #1865, #2289, .T. ) ;
#2769=FACE_OUTER_BOUND ( 'NONE', #1636, .T. ) ;
#2771=ADVANCED_FACE ( 'NONE', ( #1495 ), #10075, .F. ) ;
#2788=VERTEX_POINT ( 'NONE', #16594 ) ;
#2805=CARTESIAN_POINT ( 'NONE',  ( 0.5437965083810563094, 286.1837381376100211, 37.26905881172037027 ) ) ;
#2821=SURFACE_STYLE_USAGE ( .BOTH. , #8227 ) ;
#2837=EDGE_LOOP ( 'NONE', ( #10243, #3800, #13160, #15328 ) ) ;
#2844=ORIENTED_EDGE ( 'NONE', *, *, #4440, .F. ) ;
#2851=ORIENTED_EDGE ( 'NONE', *, *, #13303, .F. ) ;
#2852=VECTOR ( 'NONE', #4468, 1000.000000000000227 ) ;
#2866=ORIENTED_EDGE ( 'NONE', *, *, #9612, .F. ) ;
#2874=ORIENTED_EDGE ( 'NONE', *, *, #4948, .F. ) ;
#2899=CARTESIAN_POINT ( 'NONE',  ( 0.2077619023743854931, 289.4924457125955541, 37.56638074116236226 ) ) ;
#2915=CARTESIAN_POINT ( 'NONE',  ( 0.000000000000000000, 0.000000000000000000, 0.000000000000000000 ) ) ;
#2923=ORIENTED_EDGE ( 'NONE', *, *, #1183, .T. ) ;
#2958=VERTEX_POINT ( 'NONE', #10403 ) ;
#2980=CARTESIAN_POINT ( 'NONE',  ( 0.5524412557578002314, 286.1517303826834109, 37.26585803622771209 ) ) ;
#2994=ADVANCED_FACE ( 'NONE', ( #14356 ), #1219, .T. ) ;
#3002=DIRECTION ( 'NONE',  ( 6.092845550116206908E-17, -0.09950371902098546772, 0.9950371902099904853 ) ) ;
#3026=AXIS2_PLACEMENT_3D ( 'NONE', #9017, #12873, #13998 ) ;
#3069=CARTESIAN_POINT ( 'NONE',  ( -1.745738565996369118, 288.6739674670197928, 37.61874632382036765 ) ) ;
#3083=FACE_BOUND ( 'NONE', #5692, .T. ) ;
#3125=ORIENTED_EDGE ( 'NONE', *, *, #9099, .T. ) ;
#3159=CARTESIAN_POINT ( 'NONE',  ( 0.7365999999999783832, 260.4765148507123058, 287.1312267635910871 ) ) ;
#3174=CARTESIAN_POINT ( 'NONE',  ( 0.6401637624223318612, 192.7203252671974667, 37.23774918501624143 ) ) ;
#3191=VERTEX_POINT ( 'NONE', #11578 ) ;
#3196=ORIENTED_EDGE ( 'NONE', *, *, #2124, .T. ) ;
#3213=EDGE_CURVE ( 'NONE', #3191, #6345, #832, .T. ) ;
#3215=LINE ( 'NONE', #7541, #16275 ) ;
#3227=PLANE ( 'NONE',  #14920 ) ;
#3233=ORIENTED_EDGE ( 'NONE', *, *, #13636, .F. ) ;
#3280=CARTESIAN_POINT ( 'NONE',  ( 0.000000000000000000, 0.000000000000000000, 0.000000000000000000 ) ) ;
#3288=DIRECTION ( 'NONE',  ( 0.000000000000000000, 0.09950371902100227373, 0.9950371902099888199 ) ) ;
#3291=DIRECTION ( 'NONE',  ( 0.000000000000000000, -0.09950371902100807464, 0.9950371902099883759 ) ) ;
#3298=AXIS2_PLACEMENT_3D ( 'NONE', #6127, #574, #5800 ) ;
#3301=AXIS2_PLACEMENT_3D ( 'NONE', #6405, #2642, #11665 ) ;
#3314=DIRECTION ( 'NONE',  ( -4.930380657631323236E-32, 0.09950371902099770793, -0.9950371902099891530 ) ) ;
#3401=ORIENTED_EDGE ( 'NONE', *, *, #13303, .T. ) ;
#3419=CARTESIAN_POINT ( 'NONE',  ( -1.297668147409621886, 189.9512667226712779, 37.61531421653326390 ) ) ;
#3460=CARTESIAN_POINT ( 'NONE',  ( 56.72999999999999687, 289.4632308570087957, 37.52989836422092651 ) ) ;
#3539=ADVANCED_FACE ( 'NONE', ( #13979 ), #15601, .F. ) ;
#3554=CARTESIAN_POINT ( 'NONE',  ( 56.72999999999999687, 264.4632308570091368, 287.5298983642207986 ) ) ;
#3576=DIRECTION ( 'NONE',  ( 0.000000000000000000, -0.09950371902100807464, 0.9950371902099883759 ) ) ;
#3577=LINE ( 'NONE', #14298, #1179 ) ;
#3667=UNCERTAINTY_MEASURE_WITH_UNIT (LENGTH_MEASURE( 1.000000000000000082E-05 ), #15870, 'distance_accuracy_value', 'NONE');
#3697=CARTESIAN_POINT ( 'NONE',  ( -2.764312543581500581, 287.4577225941200140, 37.59778641568931334 ) ) ;
#3711=CARTESIAN_POINT ( 'NONE',  ( -3.269999999998768114, 193.4898140233619017, 37.52989836422146652 ) ) ;
#3720=ORIENTED_EDGE ( 'NONE', *, *, #1102, .F. ) ;
#3726=EDGE_CURVE ( 'NONE', #15077, #15661, #15768, .T. ) ;
#3731=DIRECTION ( 'NONE',  ( 0.000000000000000000, 0.09950371902099770793, -0.9950371902099891530 ) ) ;
#3756=EDGE_CURVE ( 'NONE', #4921, #12044, #5542, .T. ) ;
#3764=FACE_OUTER_BOUND ( 'NONE', #5292, .T. ) ;
#3773=CARTESIAN_POINT ( 'NONE',  ( -3.270000000000000462, 264.4632308570090231, 287.5298983642207986 ) ) ;
#3774=ORIENTED_EDGE ( 'NONE', *, *, #5502, .T. ) ;
#3795=VECTOR ( 'NONE', #100, 1000.000000000000114 ) ;
#3800=ORIENTED_EDGE ( 'NONE', *, *, #3726, .F. ) ;
#3820=ADVANCED_FACE ( 'NONE', ( #13549 ), #8471, .T. ) ;
#3839=LINE ( 'NONE', #14158, #13031 ) ;
#3851=DIRECTION ( 'NONE',  ( -0.000000000000000000, 2.220446049250308742E-15, 1.000000000000000000 ) ) ;
#3856=EDGE_LOOP ( 'NONE', ( #2844, #11359, #12646, #16149 ) ) ;
#3892=PLANE ( 'NONE',  #4843 ) ;
#3914=LINE ( 'NONE', #14396, #6903 ) ;
#3917=B_SPLINE_CURVE_WITH_KNOTS ( 'NONE', 3,
 ( #5962, #13544, #1776, #6995, #12327, #16438, #12253, #489, #10956, #14908 ),
 .UNSPECIFIED., .F., .F.,
 ( 4, 2, 2, 2, 4 ),
 ( 0.000000000000000000, 0.2500000000000000000, 0.5000000000000000000, 0.7500000000000000000, 1.000000000000000000 ),
 .UNSPECIFIED. ) ;
#3919=CARTESIAN_POINT ( 'NONE',  ( 0.03302700000138451830, 193.3948361422361870, 37.50583589681554741 ) ) ;
#3926=VERTEX_POINT ( 'NONE', #16367 ) ;
#4020=CARTESIAN_POINT ( 'NONE',  ( 0.7365999999999761627, 286.2094592450220034, 37.20452120302228138 ) ) ;
#4026=CARTESIAN_POINT ( 'NONE',  ( -3.270000000000000018, 220.1329686874181562, 287.5298983642209123 ) ) ;
#4066=PLANE ( 'NONE',  #13003 ) ;
#4082=ORIENTED_EDGE ( 'NONE', *, *, #2455, .F. ) ;
#4118=FACE_OUTER_BOUND ( 'NONE', #390, .T. ) ;
#4120=DIRECTION ( 'NONE',  ( 7.213771534993946619E-17, 0.09950371902098976984, 0.9950371902099900412 ) ) ;
#4131=APPLICATION_CONTEXT ( 'automotive_design' ) ;
#4147=DIRECTION ( 'NONE',  ( -1.000000000000000000, -0.000000000000000000, 0.000000000000000000 ) ) ;
#4182=EDGE_LOOP ( 'NONE', ( #11514, #9231, #12172, #16795 ) ) ;
#4185=CARTESIAN_POINT ( 'NONE',  ( 0.2839248860668147079, 286.0460148634705888, 37.35595106346542593 ) ) ;
#4193=VECTOR ( 'NONE', #6755, 1000.000000000000000 ) ;
#4232=VERTEX_POINT ( 'NONE', #12465 ) ;
#4236=CARTESIAN_POINT ( 'NONE',  ( -1.141714397801684633E-14, 214.4632308570089947, 287.5298983642209123 ) ) ;
#4247=LINE ( 'NONE', #14635, #4854 ) ;
#4279=LINE ( 'NONE', #13383, #16058 ) ;
#4304=PLANE ( 'NONE',  #5550 ) ;
#4326=ORIENTED_EDGE ( 'NONE', *, *, #7050, .F. ) ;
#4364=CARTESIAN_POINT ( 'NONE',  ( 0.7365999999999665038, 289.4632308570086252, 37.52989836422097625 ) ) ;
#4367=EDGE_LOOP ( 'NONE', ( #10143, #14132, #541, #14955 ) ) ;
#4440=EDGE_CURVE ( 'NONE', #4232, #4991, #4966, .T. ) ;
#4441=CARTESIAN_POINT ( 'NONE',  ( 1.286622718088548112E-12, 258.8496290447203023, 286.9685381829918924 ) ) ;
#4468=DIRECTION ( 'NONE',  ( 0.000000000000000000, 0.9950371902099902632, -0.09950371902098713306 ) ) ;
#4495=LINE ( 'NONE', #466, #16908 ) ;
#4527=DIRECTION ( 'NONE',  ( 3.491481338843133355E-15, -0.9950371902099891530, -0.09950371902099770793 ) ) ;
#4559=ORIENTED_EDGE ( 'NONE', *, *, #9845, .F. ) ;
#4569=CARTESIAN_POINT ( 'NONE',  ( 0.7365999999999783832, 260.4765148507123058, 287.1312267635911439 ) ) ;
#4573=ORIENTED_EDGE ( 'NONE', *, *, #16215, .T. ) ;
#4614=CARTESIAN_POINT ( 'NONE',  ( 0.01917172636759711599, 193.2913228521273368, 37.48263776190561458 ) ) ;
#4671=CARTESIAN_POINT ( 'NONE',  ( 1.250085104875786612E-12, 220.0768326692952996, 286.9685381829922903 ) ) ;
#4672=LINE ( 'NONE', #9925, #12892 ) ;
#4690=CARTESIAN_POINT ( 'NONE',  ( -3.302699999997892544, 192.9602775880926515, 37.54929111636569417 ) ) ;
#4709=CARTESIAN_POINT ( 'NONE',  ( 56.72999999999999687, 214.4632308570087957, 287.5298983642209123 ) ) ;
#4728=LINE ( 'NONE', #8523, #5645 ) ;
#4732=ORIENTED_EDGE ( 'NONE', *, *, #6292, .F. ) ;
#4747=PLANE ( 'NONE',  #1603 ) ;
#4748=CARTESIAN_POINT ( 'NONE',  ( 0.7366000000000156867, 214.4632308570090800, 287.5298983642209691 ) ) ;
#4757=EDGE_CURVE ( 'NONE', #4921, #1899, #9749, .T. ) ;
#4777=CARTESIAN_POINT ( 'NONE',  ( 0.07938566280257335073, 193.0939377745695822, 37.43526655022207450 ) ) ;
#4789=EDGE_CURVE ( 'NONE', #2788, #6952, #3839, .T. ) ;
#4803=LINE ( 'NONE', #6321, #798 ) ;
#4805=ORIENTED_EDGE ( 'NONE', *, *, #12273, .F. ) ;
#4808=DIRECTION ( 'NONE',  ( -0.000000000000000000, 0.09950371902099770793, -0.9950371902099891530 ) ) ;
#4829=VECTOR ( 'NONE', #5753, 1000.000000000000000 ) ;
#4841=VECTOR ( 'NONE', #15932, 1000.000000000000000 ) ;
#4843=AXIS2_PLACEMENT_3D ( 'NONE', #9229, #9134, #7834 ) ;
#4854=VECTOR ( 'NONE', #16089, 1000.000000000000000 ) ;
#4863=ORIENTED_EDGE ( 'NONE', *, *, #9959, .F. ) ;
#4865=CARTESIAN_POINT ( 'NONE',  ( 0.3822672831244716130, 192.8515144050814456, 37.32528944829227413 ) ) ;
#4921=VERTEX_POINT ( 'NONE', #15682 ) ;
#4948=EDGE_CURVE ( 'NONE', #12146, #14019, #4279, .T. ) ;
#4964=CARTESIAN_POINT ( 'NONE',  ( -1.725642888253134277, 288.6479481343113207, 37.61614439054953607 ) ) ;
#4966=LINE ( 'NONE', #11425, #7238 ) ;
#4991=VERTEX_POINT ( 'NONE', #11821 ) ;
#4996=DIRECTION ( 'NONE',  ( 0.000000000000000000, 0.09950371902099770793, -0.9950371902099891530 ) ) ;
#5010=CARTESIAN_POINT ( 'NONE',  ( 0.7366000000000316739, 217.7170024689957586, 287.2045212030222388 ) ) ;
#5014=ORIENTED_EDGE ( 'NONE', *, *, #10871, .F. ) ;
#5019=CARTESIAN_POINT ( 'NONE',  ( 0.7366000000000039183, 192.7170024689955028, 37.20452120302225296 ) ) ;
#5062=ORIENTED_EDGE ( 'NONE', *, *, #10871, .T. ) ;
#5065=ADVANCED_FACE ( 'NONE', ( #9514 ), #5547, .T. ) ;
#5066=CARTESIAN_POINT ( 'NONE',  ( 1.250085104875786612E-12, 218.4499468633019603, 287.1312267635915987 ) ) ;
#5118=DIRECTION ( 'NONE',  ( -3.385371974912848683E-15, -0.9950371902099904853, 0.09950371902098585630 ) ) ;
#5129=FACE_OUTER_BOUND ( 'NONE', #4367, .T. ) ;
#5174=EDGE_CURVE ( 'NONE', #15077, #10016, #15163, .T. ) ;
#5177=ORIENTED_EDGE ( 'NONE', *, *, #4948, .T. ) ;
#5189=AXIS2_PLACEMENT_3D ( 'NONE', #3159, #13789, #12584 ) ;
#5214=CARTESIAN_POINT ( 'NONE',  ( 9.454564816593551260E-13, 285.6351766110482231, 37.48264153682140432 ) ) ;
#5245=CARTESIAN_POINT ( 'NONE',  ( 1.286622718088548112E-12, 260.4765148507136701, 287.1312267635912008 ) ) ;
#5288=CARTESIAN_POINT ( 'NONE',  ( 0.01917172636707389216, 285.6351388618906526, 37.48263776190567853 ) ) ;
#5290=CARTESIAN_POINT ( 'NONE',  ( 0.7365999999999761627, 286.2094592450219466, 37.20452120302238086 ) ) ;
#5292=EDGE_LOOP ( 'NONE', ( #13203, #12313, #3125, #916 ) ) ;
#5306=CARTESIAN_POINT ( 'NONE',  ( 1.286622718088565479E-12, 285.4366476906530465, 37.52989836422118941 ) ) ;
#5320=DIRECTION ( 'NONE',  ( 6.092845550116204443E-17, 0.09950371902098714694, 0.9950371902099903743 ) ) ;
#5330=EDGE_LOOP ( 'NONE', ( #13524, #14981, #12400, #626 ) ) ;
#5341=PRODUCT_DEFINITION_FORMATION_WITH_SPECIFIED_SOURCE ( 'ANY', '', #12073, .NOT_KNOWN. ) ;
#5378=CARTESIAN_POINT ( 'NONE',  ( -1.725642888253169360, 288.6479481343113775, 37.61614439054952896 ) ) ;
#5380=AXIS2_PLACEMENT_3D ( 'NONE', #3773, #3851, #7874 ) ;
#5404=DIRECTION ( 'NONE',  ( -1.000000000000000000, 0.000000000000000000, 6.123233995736766036E-17 ) ) ;
#5459=CARTESIAN_POINT ( 'NONE',  ( -2.792885358480770019, 287.4741092055357399, 37.59942507683089019 ) ) ;
#5472=( NAMED_UNIT ( * ) SI_UNIT ( $, .STERADIAN. ) SOLID_ANGLE_UNIT ( ) );
#5486=CARTESIAN_POINT ( 'NONE',  ( 1.250085104875786612E-12, 220.0768326692952996, 286.9685381829922903 ) ) ;
#5502=EDGE_CURVE ( 'NONE', #6345, #8690, #8014, .T. ) ;
#5542=LINE ( 'NONE', #9510, #10812 ) ;
#5543=CARTESIAN_POINT ( 'NONE',  ( -3.270000000000000462, 0.000000000000000000, 0.000000000000000000 ) ) ;
#5547=PLANE ( 'NONE',  #977 ) ;
#5548=CARTESIAN_POINT ( 'NONE',  ( -2.467345170754158268, 287.9032822524807216, 37.60878752180575901 ) ) ;
#5550=AXIS2_PLACEMENT_3D ( 'NONE', #14780, #3002, #8236 ) ;
#5606=ORIENTED_EDGE ( 'NONE', *, *, #9023, .T. ) ;
#5616=CARTESIAN_POINT ( 'NONE',  ( 1.286622718088548112E-12, 260.4765148507136701, 287.1312267635912576 ) ) ;
#5645=VECTOR ( 'NONE', #3288, 1000.000000000000000 ) ;
#5692=EDGE_LOOP ( 'NONE', ( #5062, #16510 ) ) ;
#5734=LINE ( 'NONE', #12274, #8957 ) ;
#5740=DIRECTION ( 'NONE',  ( 0.000000000000000000, 0.9950371902099932608, -0.09950371902095787868 ) ) ;
#5748=DIRECTION ( 'NONE',  ( 2.920976200236518919E-15, -0.9950371902099892640, -0.09950371902099772181 ) ) ;
#5753=DIRECTION ( 'NONE',  ( -1.000000000000000000, -2.911324084205185756E-15, -2.422066625794664996E-16 ) ) ;
#5779=CARTESIAN_POINT ( 'NONE',  ( -3.270000000000000462, 285.4366476906530465, 37.52989836422091230 ) ) ;
#5789=LINE ( 'NONE', #11032, #14090 ) ;
#5800=DIRECTION ( 'NONE',  ( -3.474153781073081543E-15, -1.000000000000000000, 0.000000000000000000 ) ) ;
#5805=PLANE ( 'NONE',  #8531 ) ;
#5830=PLANE ( 'NONE',  #14340 ) ;
#5881=LINE ( 'NONE', #12496, #7135 ) ;
#5888=PLANE ( 'NONE',  #3298 ) ;
#5905=CARTESIAN_POINT ( 'NONE',  ( 0.1475654038909327559, 193.0227741332293192, 37.40882805463644445 ) ) ;
#5923=FACE_OUTER_BOUND ( 'NONE', #13338, .T. ) ;
#5925=AXIS2_PLACEMENT_3D ( 'NONE', #11168, #12708, #10131 ) ;
#5932=SHAPE_DEFINITION_REPRESENTATION ( #13598, #135 ) ;
#5936=ADVANCED_FACE ( 'NONE', ( #5129 ), #10380, .T. ) ;
#5946=CARTESIAN_POINT ( 'NONE',  ( 0.7365999999999783832, 260.4765148507123058, 287.1312267635911439 ) ) ;
#5962=CARTESIAN_POINT ( 'NONE',  ( 0.7365999999999927050, 189.4632308570089094, 37.52989836422091940 ) ) ;
#5964=ORIENTED_EDGE ( 'NONE', *, *, #7679, .F. ) ;
#5981=FACE_OUTER_BOUND ( 'NONE', #10856, .T. ) ;
#5998=EDGE_LOOP ( 'NONE', ( #7116, #1968, #13120, #1118 ) ) ;
#6060=CARTESIAN_POINT ( 'NONE',  ( 0.09296894633975227862, 193.1074002614837468, 37.43392030153066230 ) ) ;
#6084=CARTESIAN_POINT ( 'NONE',  ( -2.467345170754123185, 287.9032822524808353, 37.60878752180576612 ) ) ;
#6098=DIRECTION ( 'NONE',  ( 0.000000000000000000, 0.09950371902098545385, -0.9950371902099903743 ) ) ;
#6127=CARTESIAN_POINT ( 'NONE',  ( 56.72999999999999687, 214.4632308570087957, 287.5298983642209123 ) ) ;
#6133=ORIENTED_EDGE ( 'NONE', *, *, #9023, .F. ) ;
#6148=CARTESIAN_POINT ( 'NONE',  ( -3.269999999998768114, 193.4898140233618449, 37.52989836422147363 ) ) ;
#6155=B_SPLINE_SURFACE_WITH_KNOTS ( 'NONE', 1, 3, ( 
 ( #1433, #242, #9519, #5459, #326, #3069, #6827, #12086, #2899, #8135 ),
 ( #14577, #15940, #10539, #12265, #5548, #5378, #9427, #14757, #13557, #4364 ),
 ( #10799, #1787, #5288, #16039, #15773, #4185, #9596, #2805, #8041, #4020 ),
 ( #9258, #11919, #10625, #13302, #14672, #14497, #2719, #2980, #15856, #13384 ) ),
 .UNSPECIFIED., .F., .F., .F.,
 ( 2, 1, 1, 2 ),
 ( 4, 2, 2, 2, 4 ),
 ( -0.01000000000000000021, 0.000000000000000000, 1.000000000000000000, 1.010099999999999998 ),
 ( 0.000000000000000000, 0.2500000000000000000, 0.5000000000000000000, 0.7500000000000000000, 1.000000000000000000 ),
 .UNSPECIFIED. ) ;
#6211=EDGE_CURVE ( 'NONE', #6345, #4991, #15264, .T. ) ;
#6225=CARTESIAN_POINT ( 'NONE',  ( 0.1739760006947971005, 193.0429700394134613, 37.40680846401803450 ) ) ;
#6228=DIRECTION ( 'NONE',  ( 4.868293667060507742E-17, -0.09950371902099772181, 0.9950371902099892640 ) ) ;
#6230=EDGE_LOOP ( 'NONE', ( #10277, #16629, #8332, #13551 ) ) ;
#6274=DIRECTION ( 'NONE',  ( 6.092845550115373211E-18, 0.9950371902099904853, 0.09950371902098546772 ) ) ;
#6292=EDGE_CURVE ( 'NONE', #9971, #7606, #14201, .T. ) ;
#6311=ADVANCED_FACE ( 'NONE', ( #2769 ), #3892, .T. ) ;
#6321=CARTESIAN_POINT ( 'NONE',  ( 1.286622718088548112E-12, 258.8496290447203023, 286.9685381829918924 ) ) ;
#6345=VERTEX_POINT ( 'NONE', #5245 ) ;
#6382=CARTESIAN_POINT ( 'NONE',  ( 56.73000000000001108, 192.7170024689953891, 37.20452120302230981 ) ) ;
#6386=CARTESIAN_POINT ( 'NONE',  ( 0.5524412557582074612, 192.7747313313365112, 37.26585803622744919 ) ) ;
#6391=DIRECTION ( 'NONE',  ( -7.213771534993946619E-17, -0.09950371902098976984, -0.9950371902099900412 ) ) ;
#6405=CARTESIAN_POINT ( 'NONE',  ( 6.183064636039277557E-13, 183.8715257629572193, -18.38715257629583633 ) ) ;
#6409=ORIENTED_EDGE ( 'NONE', *, *, #10007, .F. ) ;
#6437=EDGE_CURVE ( 'NONE', #15562, #2788, #12228, .T. ) ;
#6524=ORIENTED_EDGE ( 'NONE', *, *, #3726, .T. ) ;
#6529=FACE_OUTER_BOUND ( 'NONE', #7165, .T. ) ;
#6535=EDGE_CURVE ( 'NONE', #14834, #3191, #4495, .T. ) ;
#6542=DIRECTION ( 'NONE',  ( -1.104713198929451483E-16, -0.09950371902099953980, -0.9950371902099890420 ) ) ;
#6556=EDGE_CURVE ( 'NONE', #1693, #4232, #877, .T. ) ;
#6559=EDGE_CURVE ( 'NONE', #7606, #12146, #2326, .T. ) ;
#6608=ORIENTED_EDGE ( 'NONE', *, *, #12249, .T. ) ;
#6617=CARTESIAN_POINT ( 'NONE',  ( 1.551310349710149916E-12, 193.2912851029697947, 37.48264153682136168 ) ) ;
#6634=EDGE_CURVE ( 'NONE', #12025, #3926, #4728, .T. ) ;
#6650=PLANE ( 'NONE',  #9886 ) ;
#6749=VECTOR ( 'NONE', #7132, 1000.000000000000000 ) ;
#6755=DIRECTION ( 'NONE',  ( 1.000000000000000000, 6.123233995736972804E-18, -1.353873099427978431E-32 ) ) ;
#6777=EDGE_LOOP ( 'NONE', ( #15736, #13849, #16178, #4573 ) ) ;
#6778=DIRECTION ( 'NONE',  ( 0.000000000000000000, 0.09950371902100227373, 0.9950371902099888199 ) ) ;
#6827=CARTESIAN_POINT ( 'NONE',  ( -1.297668147413691297, 288.9751949913465410, 37.61531421653335627 ) ) ;
#6870=EDGE_CURVE ( 'NONE', #10016, #14834, #14867, .T. ) ;
#6877=DIRECTION ( 'NONE',  ( 0.000000000000000000, 0.9950371902099890420, -0.09950371902099952592 ) ) ;
#6903=VECTOR ( 'NONE', #10613, 1000.000000000000000 ) ;
#6919=CARTESIAN_POINT ( 'NONE',  ( 56.73000000000001108, 239.4632308570078294, 71.73739990498292229 ) ) ;
#6952=VERTEX_POINT ( 'NONE', #15884 ) ;
#6995=CARTESIAN_POINT ( 'NONE',  ( -1.281199806751482040, 189.9796977361249048, 37.61247111518787989 ) ) ;
#7004=DIRECTION ( 'NONE',  ( -1.000000000000000000, -0.000000000000000000, 0.000000000000000000 ) ) ;
#7050=EDGE_CURVE ( 'NONE', #6952, #15054, #11328, .T. ) ;
#7087=ADVANCED_FACE ( 'NONE', ( #5923 ), #7445, .F. ) ;
#7097=CARTESIAN_POINT ( 'NONE',  ( -0.3206782292910441146, 189.5419480837538231, 37.58913636098570521 ) ) ;
#7116=ORIENTED_EDGE ( 'NONE', *, *, #16223, .F. ) ;
#7132=DIRECTION ( 'NONE',  ( 1.000000000000000000, -3.400581542615706812E-15, 2.422066625794662531E-16 ) ) ;
#7135=VECTOR ( 'NONE', #12410, 1000.000000000000000 ) ;
#7145=DIRECTION ( 'NONE',  ( 9.736587334121946093E-17, 0.09950371902099953980, 0.9950371902099891530 ) ) ;
#7165=EDGE_LOOP ( 'NONE', ( #15474, #2851, #12769, #2393 ) ) ;
#7169=CARTESIAN_POINT ( 'NONE',  ( 0.5437585709476746576, 192.7236469956751534, 37.27096646979358496 ) ) ;
#7214=ORIENTED_EDGE ( 'NONE', *, *, #4440, .T. ) ;
#7217=VECTOR ( 'NONE', #6778, 1000.000000000000000 ) ;
#7238=VECTOR ( 'NONE', #15707, 1000.000000000000227 ) ;
#7284=ORIENTED_EDGE ( 'NONE', *, *, #15167, .F. ) ;
#7309=EDGE_CURVE ( 'NONE', #7606, #8690, #5734, .T. ) ;
#7333=FACE_OUTER_BOUND ( 'NONE', #6230, .T. ) ;
#7348=CARTESIAN_POINT ( 'NONE',  ( 1.231978928595278688E-12, 193.4898140233672450, 37.52989836422093362 ) ) ;
#7354=CARTESIAN_POINT ( 'NONE',  ( 0.7366000000000293424, 218.4499468633031825, 287.1312267635914850 ) ) ;
#7371=CARTESIAN_POINT ( 'NONE',  ( -3.269999999999640750, 285.9618298588721927, 37.54886172132344768 ) ) ;
#7383=DIRECTION ( 'NONE',  ( 3.474153781073083121E-15, -1.000000000000000000, 0.000000000000000000 ) ) ;
#7427=CARTESIAN_POINT ( 'NONE',  ( -1.281199806751509129, 189.9796977361249617, 37.61247111518789410 ) ) ;
#7445=CYLINDRICAL_SURFACE ( 'NONE', #5925, 15.00000000000000000 ) ;
#7491=LINE ( 'NONE', #8467, #9405 ) ;
#7511=ADVANCED_FACE ( 'NONE', ( #5981 ), #2597, .F. ) ;
#7516=CARTESIAN_POINT ( 'NONE',  ( 56.72999999999999687, 189.4632308570086536, 37.52989836422099046 ) ) ;
#7535=DIRECTION ( 'NONE',  ( -3.407805566942604749E-15, -0.9950371902099890420, 0.09950371902099952592 ) ) ;
#7536=CARTESIAN_POINT ( 'NONE',  ( 0.7365999999999666148, 289.4632308570086252, 37.52989836422091230 ) ) ;
#7541=CARTESIAN_POINT ( 'NONE',  ( 56.73000000000001108, 286.2094592450221739, 37.20452120302226007 ) ) ;
#7557=ORIENTED_EDGE ( 'NONE', *, *, #12250, .F. ) ;
#7592=DIRECTION ( 'NONE',  ( 0.000000000000000000, -0.9950371902099879318, -0.09950371902101125265 ) ) ;
#7601=( GEOMETRIC_REPRESENTATION_CONTEXT ( 3 ) GLOBAL_UNCERTAINTY_ASSIGNED_CONTEXT ( ( #3667 ) ) GLOBAL_UNIT_ASSIGNED_CONTEXT ( ( #15870, #10982, #5472 ) ) REPRESENTATION_CONTEXT ( 'NONE', 'WORKASPACE' ) );
#7605=FACE_BOUND ( 'NONE', #14455, .T. ) ;
#7606=VERTEX_POINT ( 'NONE', #8996 ) ;
#7630=APPLICATION_CONTEXT ( 'automotive_design' ) ;
#7635=LINE ( 'NONE', #5066, #1670 ) ;
#7660=ORIENTED_EDGE ( 'NONE', *, *, #6559, .T. ) ;
#7670=DIRECTION ( 'NONE',  ( -2.920976200236518919E-15, 0.9950371902099891530, 0.09950371902099770793 ) ) ;
#7679=EDGE_CURVE ( 'NONE', #997, #9809, #14748, .T. ) ;
#7681=DIRECTION ( 'NONE',  ( 0.000000000000000000, -0.9950371902099891530, -0.09950371902099770793 ) ) ;
#7683=EDGE_LOOP ( 'NONE', ( #8209, #2632, #13381, #15537 ) ) ;
#7782=ORIENTED_EDGE ( 'NONE', *, *, #6556, .F. ) ;
#7783=CIRCLE ( 'NONE', #11879, 4.006599999998782913 ) ;
#7808=CARTESIAN_POINT ( 'NONE',  ( 56.73000000000000398, 261.2094592450224582, 287.2045212030221251 ) ) ;
#7834=DIRECTION ( 'NONE',  ( 0.000000000000000000, 0.09950371902099953980, 0.9950371902099890420 ) ) ;
#7874=DIRECTION ( 'NONE',  ( 0.000000000000000000, -1.000000000000000000, 2.220446049250308742E-15 ) ) ;
#7896=CARTESIAN_POINT ( 'NONE',  ( -3.270000000000002238, 239.4632308570078294, 56.73739990498292940 ) ) ;
#7933=CARTESIAN_POINT ( 'NONE',  ( 56.73000000000001108, 286.2094592450221739, 37.20452120302225296 ) ) ;
#7983=ORIENTED_EDGE ( 'NONE', *, *, #16211, .T. ) ;
#8014=LINE ( 'NONE', #5616, #14151 ) ;
#8041=CARTESIAN_POINT ( 'NONE',  ( 0.6401637624220996026, 286.2061364468225975, 37.23774918501653985 ) ) ;
#8061=FACE_OUTER_BOUND ( 'NONE', #16789, .T. ) ;
#8067=FACE_OUTER_BOUND ( 'NONE', #3856, .T. ) ;
#8072=CARTESIAN_POINT ( 'NONE',  ( 0.7366000000000293424, 218.4499468633031825, 287.1312267635914850 ) ) ;
#8075=DIRECTION ( 'NONE',  ( 0.000000000000000000, 0.000000000000000000, 1.000000000000000000 ) ) ;
#8092=EDGE_CURVE ( 'NONE', #7606, #4921, #4247, .T. ) ;
#8107=LINE ( 'NONE', #14731, #16468 ) ;
#8108=ORIENTED_EDGE ( 'NONE', *, *, #12249, .F. ) ;
#8135=CARTESIAN_POINT ( 'NONE',  ( 0.7365999999999663927, 289.4957685731285437, 37.53315213583296384 ) ) ;
#8152=DIRECTION ( 'NONE',  ( -1.000000000000000000, -0.000000000000000000, 0.000000000000000000 ) ) ;
#8207=DIRECTION ( 'NONE',  ( 6.092845550116402428E-18, -0.9950371902099888199, 0.09950371902100227373 ) ) ;
#8209=ORIENTED_EDGE ( 'NONE', *, *, #12571, .T. ) ;
#8211=DIRECTION ( 'NONE',  ( 0.000000000000000000, -2.081668171172169746E-16, -1.000000000000000000 ) ) ;
#8215=DIRECTION ( 'NONE',  ( -2.920976200236483125E-16, 0.09950371902099772181, -0.9950371902099892640 ) ) ;
#8227=SURFACE_SIDE_STYLE ('',( #14850 ) ) ;
#8236=DIRECTION ( 'NONE',  ( 0.000000000000000000, -0.9950371902099903743, -0.09950371902098545385 ) ) ;
#8272=CARTESIAN_POINT ( 'NONE',  ( 0.000000000000000000, 239.4632308570078294, 86.73739990498292229 ) ) ;
#8304=DIRECTION ( 'NONE',  ( 0.000000000000000000, 0.9950371902099903743, 0.09950371902098545385 ) ) ;
#8319=PRESENTATION_STYLE_ASSIGNMENT (( #2821 ) ) ;
#8332=ORIENTED_EDGE ( 'NONE', *, *, #9845, .T. ) ;
#8359=FACE_OUTER_BOUND ( 'NONE', #8818, .T. ) ;
#8367=LINE ( 'NONE', #15999, #15711 ) ;
#8410=CARTESIAN_POINT ( 'NONE',  ( -3.302699999998768288, 193.4898140233617880, 37.52989836422148073 ) ) ;
#8467=CARTESIAN_POINT ( 'NONE',  ( -3.270000000000000462, 264.4632308570090231, 287.5298983642207986 ) ) ;
#8471=PLANE ( 'NONE',  #2296 ) ;
#8480=CARTESIAN_POINT ( 'NONE',  ( 56.73000000000001108, 217.7170024689955596, 287.2045212030222388 ) ) ;
#8488=CARTESIAN_POINT ( 'NONE',  ( -0.3121190734725042826, 189.5736389302157647, 37.58596727633950252 ) ) ;
#8493=MANIFOLD_SOLID_BREP ( 'Cut-Extrude1', #13760 ) ;
#8503=LINE ( 'NONE', #12704, #2852 ) ;
#8508=ORIENTED_EDGE ( 'NONE', *, *, #10392, .F. ) ;
#8523=CARTESIAN_POINT ( 'NONE',  ( -3.270000000000000462, 189.4851275752425295, -18.94851275752489883 ) ) ;
#8531=AXIS2_PLACEMENT_3D ( 'NONE', #14758, #8215, #12267 ) ;
#8537=DIRECTION ( 'NONE',  ( 0.000000000000000000, -0.9950371902099890420, 0.09950371902099952592 ) ) ;
#8557=ADVANCED_BREP_SHAPE_REPRESENTATION ( '', ( #8493, #1488 ), #2021 ) ;
#8682=EDGE_CURVE ( 'NONE', #15562, #11437, #11652, .T. ) ;
#8690=VERTEX_POINT ( 'NONE', #1173 ) ;
#8693=DIRECTION ( 'NONE',  ( 0.000000000000000000, 0.000000000000000000, 1.000000000000000000 ) ) ;
#8734=CARTESIAN_POINT ( 'NONE',  ( -3.270000000000000462, 285.4366476906530465, 37.52989836422091230 ) ) ;
#8743=CARTESIAN_POINT ( 'NONE',  ( 0.7365999999999711667, 189.4632308570113537, 37.52989836422062808 ) ) ;
#8770=ADVANCED_FACE ( 'NONE', ( #3764 ), #12935, .F. ) ;
#8796=DIRECTION ( 'NONE',  ( 0.000000000000000000, -0.09950371902098545385, 0.9950371902099903743 ) ) ;
#8818=EDGE_LOOP ( 'NONE', ( #13886, #4559, #5606, #3720 ) ) ;
#8821=LINE ( 'NONE', #844, #15960 ) ;
#8824=ADVANCED_FACE ( 'NONE', ( #7605, #15769 ), #6650, .T. ) ;
#8841=DIRECTION ( 'NONE',  ( 3.491481338843132566E-15, 0.9950371902099890420, -0.09950371902099952592 ) ) ;
#8914=CARTESIAN_POINT ( 'NONE',  ( 0.6444877810228004655, 192.7531883598551872, 37.23446286945478079 ) ) ;
#8951=ORIENTED_EDGE ( 'NONE', *, *, #12341, .F. ) ;
#8957=VECTOR ( 'NONE', #13479, 1000.000000000000000 ) ;
#8981=ADVANCED_FACE ( 'NONE', ( #7333 ), #12669, .F. ) ;
#8996=CARTESIAN_POINT ( 'NONE',  ( 1.231993379943791155E-12, 193.4898140233672450, 37.52989836422092651 ) ) ;
#9005=ADVANCED_FACE ( 'NONE', ( #15076 ), #5888, .F. ) ;
#9017=CARTESIAN_POINT ( 'NONE',  ( 0.7365999999999783832, 260.4765148507123058, 287.1312267635910871 ) ) ;
#9023=EDGE_CURVE ( 'NONE', #11441, #15661, #4672, .T. ) ;
#9062=DIRECTION ( 'NONE',  ( -3.407805566942604749E-15, -0.9950371902099890420, 0.09950371902099952592 ) ) ;
#9074=CARTESIAN_POINT ( 'NONE',  ( 0.7366000000000204606, 214.4632308570090800, 287.5298983642209123 ) ) ;
#9089=FACE_OUTER_BOUND ( 'NONE', #4182, .T. ) ;
#9099=EDGE_CURVE ( 'NONE', #1899, #9971, #2432, .T. ) ;
#9105=CARTESIAN_POINT ( 'NONE',  ( 56.73000000000001108, 192.7170024689953891, 37.20452120302224586 ) ) ;
#9134=DIRECTION ( 'NONE',  ( 3.407805566942604354E-15, 0.9950371902099891530, -0.09950371902099955368 ) ) ;
#9166=AXIS2_PLACEMENT_3D ( 'NONE', #4569, #12224, #11100 ) ;
#9228=EDGE_CURVE ( 'NONE', #11441, #14417, #8107, .T. ) ;
#9229=CARTESIAN_POINT ( 'NONE',  ( 6.297236075819447898E-13, 187.1252973749438695, -18.71252973749450632 ) ) ;
#9231=ORIENTED_EDGE ( 'NONE', *, *, #6437, .T. ) ;
#9258=CARTESIAN_POINT ( 'NONE',  ( 0.03302700000128662439, 285.4366476906504317, 37.52989836422092651 ) ) ;
#9279=CARTESIAN_POINT ( 'NONE',  ( -3.270000000000000462, 218.4499468633019603, 287.1312267635915987 ) ) ;
#9313=ORIENTED_EDGE ( 'NONE', *, *, #1102, .T. ) ;
#9317=EDGE_CURVE ( 'NONE', #4921, #16177, #7635, .T. ) ;
#9320=ORIENTED_EDGE ( 'NONE', *, *, #7309, .F. ) ;
#9322=DIRECTION ( 'NONE',  ( 0.000000000000000000, 0.09950371902098545385, -0.9950371902099903743 ) ) ;
#9405=VECTOR ( 'NONE', #1927, 1000.000000000000000 ) ;
#9427=CARTESIAN_POINT ( 'NONE',  ( -1.281199806755545456, 288.9467639778928856, 37.61247111518799358 ) ) ;
#9430=VECTOR ( 'NONE', #10998, 1000.000000000000000 ) ;
#9471=AXIS2_PLACEMENT_3D ( 'NONE', #2204, #6228, #7681 ) ;
#9510=CARTESIAN_POINT ( 'NONE',  ( 1.250085104875786612E-12, 218.4499468633019603, 287.1312267635915987 ) ) ;
#9514=FACE_OUTER_BOUND ( 'NONE', #14447, .T. ) ;
#9519=CARTESIAN_POINT ( 'NONE',  ( -3.197567832866743398, 286.4953233758678834, 37.56865621330340588 ) ) ;
#9543=DIRECTION ( 'NONE',  ( 0.000000000000000000, -0.9950371902099902632, 0.09950371902098713306 ) ) ;
#9548=LINE ( 'NONE', #11855, #3795 ) ;
#9573=ORIENTED_EDGE ( 'NONE', *, *, #2763, .F. ) ;
#9596=CARTESIAN_POINT ( 'NONE',  ( 0.3656342590590464514, 286.1036626325263796, 37.32816098065131882 ) ) ;
#9599=ORIENTED_EDGE ( 'NONE', *, *, #16223, .T. ) ;
#9612=EDGE_CURVE ( 'NONE', #15922, #6345, #1610, .T. ) ;
#9614=FILL_AREA_STYLE ('',( #10814 ) ) ;
#9639=ORIENTED_EDGE ( 'NONE', *, *, #14392, .F. ) ;
#9676=ADVANCED_FACE ( 'NONE', ( #12179 ), #5805, .F. ) ;
#9699=CARTESIAN_POINT ( 'NONE',  ( -2.493494276495503037, 191.0031835148159303, 37.61078711647776629 ) ) ;
#9712=ADVANCED_FACE ( 'NONE', ( #13471 ), #13385, .F. ) ;
#9720=VECTOR ( 'NONE', #2629, 1000.000000000000000 ) ;
#9747=CARTESIAN_POINT ( 'NONE',  ( 6.237780304489215888E-13, 189.4632308570089094, 37.52989836422088388 ) ) ;
#9749=CIRCLE ( 'NONE', #2319, 0.7365999999987737912 ) ;
#9786=CARTESIAN_POINT ( 'NONE',  ( 0.5437965083814821909, 192.7427235764099578, 37.26905881172010737 ) ) ;
#9790=ORIENTED_EDGE ( 'NONE', *, *, #2090, .F. ) ;
#9801=ORIENTED_EDGE ( 'NONE', *, *, #10766, .T. ) ;
#9809=VERTEX_POINT ( 'NONE', #12844 ) ;
#9845=EDGE_CURVE ( 'NONE', #11441, #4991, #10438, .T. ) ;
#9862=CARTESIAN_POINT ( 'NONE',  ( 0.7366000000000042514, 192.7498655622790977, 37.20123489369387926 ) ) ;
#9886=AXIS2_PLACEMENT_3D ( 'NONE', #5543, #7004, #10793 ) ;
#9899=CARTESIAN_POINT ( 'NONE',  ( -3.270000000000000462, 284.6994879831845537, 28.46994879831456515 ) ) ;
#9925=CARTESIAN_POINT ( 'NONE',  ( 0.7365999999999666148, 289.4632308570086252, 37.52989836422090519 ) ) ;
#9947=CARTESIAN_POINT ( 'NONE',  ( 0.2120431089105883071, 189.4665537169271374, 37.56312696337839441 ) ) ;
#9959=EDGE_CURVE ( 'NONE', #1511, #15922, #15757, .T. ) ;
#9971=VERTEX_POINT ( 'NONE', #1076 ) ;
#9979=( NAMED_UNIT ( * ) SI_UNIT ( $, .STERADIAN. ) SOLID_ANGLE_UNIT ( ) );
#9987=FACE_OUTER_BOUND ( 'NONE', #5330, .T. ) ;
#9990=AXIS2_PLACEMENT_3D ( 'NONE', #5946, #3291, #15051 ) ;
#10005=CARTESIAN_POINT ( 'NONE',  ( 0.7365999999999666148, 264.4632308570089663, 287.5298983642207986 ) ) ;
#10007=EDGE_CURVE ( 'NONE', #9971, #15562, #10433, .T. ) ;
#10016=VERTEX_POINT ( 'NONE', #7933 ) ;
#10075=CYLINDRICAL_SURFACE ( 'NONE', #9990, 0.7365999999986965197 ) ;
#10101=ORIENTED_EDGE ( 'NONE', *, *, #6559, .F. ) ;
#10116=ORIENTED_EDGE ( 'NONE', *, *, #7309, .T. ) ;
#10131=DIRECTION ( 'NONE',  ( 0.000000000000000000, 0.000000000000000000, 1.000000000000000000 ) ) ;
#10143=ORIENTED_EDGE ( 'NONE', *, *, #2455, .T. ) ;
#10159=ORIENTED_EDGE ( 'NONE', *, *, #6437, .F. ) ;
#10165=DIRECTION ( 'NONE',  ( -0.000000000000000000, 0.09950371902100807464, -0.9950371902099882648 ) ) ;
#10214=EDGE_LOOP ( 'NONE', ( #8508, #15651, #3196, #7782 ) ) ;
#10218=CARTESIAN_POINT ( 'NONE',  ( -0.3121190734747608664, 289.3528227838038447, 37.58596727633977963 ) ) ;
#10243=ORIENTED_EDGE ( 'NONE', *, *, #2090, .T. ) ;
#10259=PLANE ( 'NONE',  #109 ) ;
#10277=ORIENTED_EDGE ( 'NONE', *, *, #3213, .F. ) ;
#10288=CARTESIAN_POINT ( 'NONE',  ( 0.03302700000123198060, 193.4898140233673018, 37.52989836422092651 ) ) ;
#10312=EDGE_LOOP ( 'NONE', ( #14625, #4326, #2436, #2758 ) ) ;
#10338=ORIENTED_EDGE ( 'NONE', *, *, #15567, .F. ) ;
#10380=PLANE ( 'NONE',  #5380 ) ;
#10383=DIRECTION ( 'NONE',  ( -2.920976200236518919E-15, 0.9950371902099891530, 0.09950371902099770793 ) ) ;
#10392=EDGE_CURVE ( 'NONE', #1511, #1693, #14461, .T. ) ;
#10403=CARTESIAN_POINT ( 'NONE',  ( 1.250085104875786612E-12, 220.1329686874181562, 287.5298983642209123 ) ) ;
#10410=ADVANCED_FACE ( 'NONE', ( #6529 ), #14280, .T. ) ;
#10430=EDGE_CURVE ( 'NONE', #14417, #15077, #1307, .T. ) ;
#10433=LINE ( 'NONE', #5019, #14853 ) ;
#10436=CARTESIAN_POINT ( 'NONE',  ( 0.000000000000000000, 258.7934930265975026, 287.5298983642207986 ) ) ;
#10438=CIRCLE ( 'NONE', #13195, 4.006599999998678108 ) ;
#10539=CARTESIAN_POINT ( 'NONE',  ( -3.165718926339676109, 286.4868066975116676, 37.56780454546778714 ) ) ;
#10563=DIRECTION ( 'NONE',  ( 1.000000000000000000, -3.400581542615706812E-15, 2.422066625794662531E-16 ) ) ;
#10613=DIRECTION ( 'NONE',  ( -1.000000000000000000, -0.000000000000000000, -0.000000000000000000 ) ) ;
#10624=PRODUCT_DEFINITION ( 'UNKNOWN', '', #5341, #15316 ) ;
#10625=CARTESIAN_POINT ( 'NONE',  ( 0.05133912195941206513, 285.6265370167508877, 37.48177757739169635 ) ) ;
#10638=CARTESIAN_POINT ( 'NONE',  ( 0.3521046271551984685, 286.1171785048110792, 37.32951256787983851 ) ) ;
#10710=EDGE_LOOP ( 'NONE', ( #3774, #2923, #2684, #15627 ) ) ;
#10765=ORIENTED_EDGE ( 'NONE', *, *, #16211, .F. ) ;
#10766=EDGE_CURVE ( 'NONE', #12146, #16177, #14095, .T. ) ;
#10793=DIRECTION ( 'NONE',  ( 0.000000000000000000, 0.000000000000000000, 1.000000000000000000 ) ) ;
#10796=CARTESIAN_POINT ( 'NONE',  ( -3.270000000000000462, 289.4632308570086821, 37.52989836422091230 ) ) ;
#10799=CARTESIAN_POINT ( 'NONE',  ( 1.286622718088548112E-12, 285.4366476906503749, 37.52989836422091940 ) ) ;
#10802=AXIS2_PLACEMENT_3D ( 'NONE', #14787, #15972, #8075 ) ;
#10812=VECTOR ( 'NONE', #13201, 1000.000000000000114 ) ;
#10814=FILL_AREA_STYLE_COLOUR ( '', #2683 ) ;
#10826=PLANE ( 'NONE',  #14324 ) ;
#10846=DIRECTION ( 'NONE',  ( -3.407805566942625851E-16, -0.09950371902099953980, -0.9950371902099891530 ) ) ;
#10856=EDGE_LOOP ( 'NONE', ( #4732, #13722, #3401, #10101 ) ) ;
#10871=EDGE_CURVE ( 'NONE', #997, #12302, #13777, .T. ) ;
#10927=ADVANCED_FACE ( 'NONE', ( #4118 ), #10826, .T. ) ;
#10956=CARTESIAN_POINT ( 'NONE',  ( -3.269999999997899476, 192.9646318551354227, 37.54886172132446376 ) ) ;
#10982=( NAMED_UNIT ( * ) PLANE_ANGLE_UNIT ( ) SI_UNIT ( $, .RADIAN. ) );
#10989=VECTOR ( 'NONE', #6542, 1000.000000000000227 ) ;
#10998=DIRECTION ( 'NONE',  ( -1.000000000000000000, 3.424802208873653704E-15, 9.809413627650283915E-33 ) ) ;
#11011=VECTOR ( 'NONE', #9322, 1000.000000000000227 ) ;
#11032=CARTESIAN_POINT ( 'NONE',  ( 1.286622718088548112E-12, 285.4366476906530465, 37.52989836422116099 ) ) ;
#11077=ADVANCED_FACE ( 'NONE', ( #854 ), #5830, .T. ) ;
#11100=DIRECTION ( 'NONE',  ( -2.922523701604180730E-15, 0.9950371902099879318, 0.09950371902101125265 ) ) ;
#11168=CARTESIAN_POINT ( 'NONE',  ( 56.73000000000001108, 239.4632308570078294, 71.73739990498292229 ) ) ;
#11183=CARTESIAN_POINT ( 'NONE',  ( 1.232007831292310690E-12, 193.4898140233672450, 37.52989836422092651 ) ) ;
#11237=VERTEX_POINT ( 'NONE', #15535 ) ;
#11321=CARTESIAN_POINT ( 'NONE',  ( -8.522270667398414726E-13, 287.0593181834893244, 28.70593181834858498 ) ) ;
#11328=LINE ( 'NONE', #4709, #1265 ) ;
#11332=CARTESIAN_POINT ( 'NONE',  ( 0.7365999999999665038, 289.4632308570086252, 37.52989836422111125 ) ) ;
#11333=ORIENTED_EDGE ( 'NONE', *, *, #9228, .F. ) ;
#11359=ORIENTED_EDGE ( 'NONE', *, *, #2124, .F. ) ;
#11385=EDGE_CURVE ( 'NONE', #3926, #2958, #15947, .T. ) ;
#11425=CARTESIAN_POINT ( 'NONE',  ( -3.270000000000000462, -25.84985893846420169, 258.4985893846773592 ) ) ;
#11437=VERTEX_POINT ( 'NONE', #4748 ) ;
#11441=VERTEX_POINT ( 'NONE', #10005 ) ;
#11448=CARTESIAN_POINT ( 'NONE',  ( 0.7365999999999665038, 289.4632308570086252, 37.52989836422111125 ) ) ;
#11491=CARTESIAN_POINT ( 'NONE',  ( 0.7366000000000204606, 214.4632308570089947, 287.5298983642209123 ) ) ;
#11514=ORIENTED_EDGE ( 'NONE', *, *, #8682, .F. ) ;
#11528=DIRECTION ( 'NONE',  ( -1.000000000000000000, 6.123233995735932031E-18, -1.353873099427752636E-32 ) ) ;
#11578=CARTESIAN_POINT ( 'NONE',  ( 0.7365999999999761627, 261.2094592450197297, 287.2045212030218408 ) ) ;
#11652=LINE ( 'NONE', #9074, #12826 ) ;
#11665=DIRECTION ( 'NONE',  ( 0.000000000000000000, 0.09950371902099953980, 0.9950371902099890420 ) ) ;
#11674=VECTOR ( 'NONE', #1989, 1000.000000000000000 ) ;
#11691=DIRECTION ( 'NONE',  ( 7.213771534993947851E-17, 0.09950371902098976984, 0.9950371902099900412 ) ) ;
#11701=CARTESIAN_POINT ( 'NONE',  ( 0.7366000000000112458, 193.4499468633054846, 37.13122676359123631 ) ) ;
#11730=B_SPLINE_CURVE_WITH_KNOTS ( 'NONE', 3,
 ( #5306, #5214, #2474, #10638, #86, #15622 ),
 .UNSPECIFIED., .F., .F.,
 ( 4, 2, 4 ),
 ( 0.000000000000000000, 0.5000000000000000000, 1.000000000000000000 ),
 .UNSPECIFIED. ) ;
#11739=CARTESIAN_POINT ( 'NONE',  ( 0.7366000000000112458, 193.4499468633054846, 37.13122676359123631 ) ) ;
#11781=DIRECTION ( 'NONE',  ( -7.213771534993946619E-17, -0.09950371902098976984, -0.9950371902099900412 ) ) ;
#11803=EDGE_LOOP ( 'NONE', ( #2874, #9801, #13746, #2206, #4082, #12936, #7214, #2122 ) ) ;
#11821=CARTESIAN_POINT ( 'NONE',  ( -3.269999999998713491, 260.4765148507195249, 287.1312267635918261 ) ) ;
#11855=CARTESIAN_POINT ( 'NONE',  ( 56.72999999999999687, 264.4632308570091368, 287.5298983642207986 ) ) ;
#11879=AXIS2_PLACEMENT_3D ( 'NONE', #8072, #4120, #15714 ) ;
#11919=CARTESIAN_POINT ( 'NONE',  ( 0.03302700000112353956, 285.5316255717817171, 37.50583589681555452 ) ) ;
#11981=ORIENTED_EDGE ( 'NONE', *, *, #11385, .F. ) ;
#12025=VERTEX_POINT ( 'NONE', #874 ) ;
#12027=UNCERTAINTY_MEASURE_WITH_UNIT (LENGTH_MEASURE( 1.000000000000000082E-05 ), #12468, 'distance_accuracy_value', 'NONE');
#12029=DIRECTION ( 'NONE',  ( 1.000000000000000000, 2.935544750463131859E-15, 4.905671055753177464E-32 ) ) ;
#12031=ADVANCED_FACE ( 'NONE', ( #9987 ), #13936, .F. ) ;
#12044=VERTEX_POINT ( 'NONE', #13147 ) ;
#12073=PRODUCT ( 'Part2', 'Part2', '', ( #16582 ) ) ;
#12080=VECTOR ( 'NONE', #7535, 1000.000000000000227 ) ;
#12086=CARTESIAN_POINT ( 'NONE',  ( -0.3206782292933404999, 289.3845136302657579, 37.58913636098598232 ) ) ;
#12146=VERTEX_POINT ( 'NONE', #3711 ) ;
#12148=DIRECTION ( 'NONE',  ( 1.000000000000000000, 2.935544750463131859E-15, 4.954244443042633456E-32 ) ) ;
#12172=ORIENTED_EDGE ( 'NONE', *, *, #4789, .T. ) ;
#12179=FACE_OUTER_BOUND ( 'NONE', #712, .T. ) ;
#12208=CARTESIAN_POINT ( 'NONE',  ( 0.000000000000000000, 239.4632308570078294, 56.73739990498292940 ) ) ;
#12224=DIRECTION ( 'NONE',  ( 0.000000000000000000, -0.09950371902100807464, 0.9950371902099883759 ) ) ;
#12228=LINE ( 'NONE', #9747, #6749 ) ;
#12231=DIRECTION ( 'NONE',  ( 0.000000000000000000, 0.000000000000000000, 1.000000000000000000 ) ) ;
#12249=EDGE_CURVE ( 'NONE', #12044, #2958, #16228, .T. ) ;
#12250=EDGE_CURVE ( 'NONE', #15054, #1899, #14520, .T. ) ;
#12253=CARTESIAN_POINT ( 'NONE',  ( -2.764312543576804337, 191.4687391198921205, 37.59778641568980362 ) ) ;
#12263=CARTESIAN_POINT ( 'NONE',  ( 56.72999999999999687, 289.4632308570088526, 37.52989836422092651 ) ) ;
#12265=CARTESIAN_POINT ( 'NONE',  ( -2.764312543581565418, 287.4577225941199004, 37.59778641568930624 ) ) ;
#12267=DIRECTION ( 'NONE',  ( 0.000000000000000000, 0.9950371902099891530, 0.09950371902099770793 ) ) ;
#12273=EDGE_CURVE ( 'NONE', #1865, #9809, #1197, .T. ) ;
#12274=CARTESIAN_POINT ( 'NONE',  ( 0.000000000000000000, 289.4632308570086821, 37.52989836422091230 ) ) ;
#12291=CARTESIAN_POINT ( 'NONE',  ( -1.865551803243643184E-15, 286.2094592450220034, 37.20452120302224586 ) ) ;
#12302=VERTEX_POINT ( 'NONE', #12208 ) ;
#12313=ORIENTED_EDGE ( 'NONE', *, *, #4757, .T. ) ;
#12327=CARTESIAN_POINT ( 'NONE',  ( -1.725642888248489104, 190.2785135797052760, 37.61614439054951475 ) ) ;
#12341=EDGE_CURVE ( 'NONE', #16177, #12025, #8503, .T. ) ;
#12345=AXIS2_PLACEMENT_3D ( 'NONE', #11739, #6391, #5118 ) ;
#12349=VECTOR ( 'NONE', #12775, 1000.000000000000227 ) ;
#12350=CARTESIAN_POINT ( 'NONE',  ( -2.467345170749102312, 191.0231794615329193, 37.60878752180607165 ) ) ;
#12374=VECTOR ( 'NONE', #8304, 1000.000000000000114 ) ;
#12399=ORIENTED_EDGE ( 'NONE', *, *, #9317, .F. ) ;
#12400=ORIENTED_EDGE ( 'NONE', *, *, #10430, .F. ) ;
#12410=DIRECTION ( 'NONE',  ( 0.000000000000000000, -1.000000000000000000, 2.220446049250308742E-15 ) ) ;
#12429=CARTESIAN_POINT ( 'NONE',  ( 0.3521046271560109298, 192.8092832092085587, 37.32951256787957561 ) ) ;
#12432=CARTESIAN_POINT ( 'NONE',  ( 0.2077619023754708749, 189.4340160014244248, 37.56638074116201409 ) ) ;
#12465=CARTESIAN_POINT ( 'NONE',  ( -3.270000000000000462, 258.8496290447203592, 286.9685381829918924 ) ) ;
#12468=( LENGTH_UNIT ( ) NAMED_UNIT ( * ) SI_UNIT ( .MILLI., .METRE. ) );
#12496=CARTESIAN_POINT ( 'NONE',  ( 0.000000000000000000, 264.4632308570090231, 287.5298983642207986 ) ) ;
#12509=CARTESIAN_POINT ( 'NONE',  ( 0.7365999999999783832, 260.4765148507123058, 287.1312267635910871 ) ) ;
#12510=CARTESIAN_POINT ( 'NONE',  ( 56.72999999999999687, 289.4632308570087957, 37.52989836422092651 ) ) ;
#12543=ORIENTED_EDGE ( 'NONE', *, *, #12273, .T. ) ;
#12571=EDGE_CURVE ( 'NONE', #1899, #11437, #14418, .T. ) ;
#12584=DIRECTION ( 'NONE',  ( 0.000000000000000000, 0.9950371902099882648, 0.09950371902100807464 ) ) ;
#12611=ADVANCED_FACE ( 'NONE', ( #9089 ), #16807, .F. ) ;
#12623=EDGE_LOOP ( 'NONE', ( #6133, #2244, #12884, #6524 ) ) ;
#12646=ORIENTED_EDGE ( 'NONE', *, *, #9612, .T. ) ;
#12655=CARTESIAN_POINT ( 'NONE',  ( -3.270000000000000462, 258.7934930265975026, 287.5298983642207986 ) ) ;
#12669=PLANE ( 'NONE',  #5189 ) ;
#12704=CARTESIAN_POINT ( 'NONE',  ( -3.270000000000000462, 30.59170509404782479, 305.9170509405147982 ) ) ;
#12708=DIRECTION ( 'NONE',  ( -1.000000000000000000, -0.000000000000000000, -0.000000000000000000 ) ) ;
#12713=CARTESIAN_POINT ( 'NONE',  ( -3.165718926339639694, 286.4868066975118381, 37.56780454546780845 ) ) ;
#12769=ORIENTED_EDGE ( 'NONE', *, *, #8682, .T. ) ;
#12775=DIRECTION ( 'NONE',  ( 3.491481338843132566E-15, 0.9950371902099890420, -0.09950371902099952592 ) ) ;
#12777=CARTESIAN_POINT ( 'NONE',  ( 0.1218274893879093684, 193.1239507390138215, 37.43226525377765768 ) ) ;
#12780=DIRECTION ( 'NONE',  ( 1.104713198929451483E-16, 0.09950371902099953980, 0.9950371902099890420 ) ) ;
#12816=DIRECTION ( 'NONE',  ( 0.000000000000000000, -0.9950371902099900412, 0.09950371902098976984 ) ) ;
#12826=VECTOR ( 'NONE', #12780, 1000.000000000000227 ) ;
#12844=CARTESIAN_POINT ( 'NONE',  ( -3.270000000000002238, 239.4632308570078294, 86.73739990498292229 ) ) ;
#12873=DIRECTION ( 'NONE',  ( 0.000000000000000000, -0.09950371902100807464, 0.9950371902099883759 ) ) ;
#12884=ORIENTED_EDGE ( 'NONE', *, *, #10430, .T. ) ;
#12892=VECTOR ( 'NONE', #3314, 1000.000000000000114 ) ;
#12929=LINE ( 'NONE', #7516, #12349 ) ;
#12935=CYLINDRICAL_SURFACE ( 'NONE', #12345, 0.7365999999987759006 ) ;
#12936=ORIENTED_EDGE ( 'NONE', *, *, #6556, .T. ) ;
#12947=ORIENTED_EDGE ( 'NONE', *, *, #5502, .F. ) ;
#12966=EDGE_CURVE ( 'NONE', #2788, #1418, #12929, .T. ) ;
#12977=DIRECTION ( 'NONE',  ( -1.000000000000000000, -1.672079375435207996E-12, 1.507226479265539607E-13 ) ) ;
#13003=AXIS2_PLACEMENT_3D ( 'NONE', #4236, #10846, #6877 ) ;
#13006=EDGE_LOOP ( 'NONE', ( #11981, #15427, #10765, #6608 ) ) ;
#13031=VECTOR ( 'NONE', #2378, 1000.000000000000227 ) ;
#13120=ORIENTED_EDGE ( 'NONE', *, *, #6870, .F. ) ;
#13147=CARTESIAN_POINT ( 'NONE',  ( 1.250085104875786612E-12, 220.0768326692952996, 286.9685381829922903 ) ) ;
#13160=ORIENTED_EDGE ( 'NONE', *, *, #5174, .T. ) ;
#13181=ORIENTED_EDGE ( 'NONE', *, *, #7679, .T. ) ;
#13189=CARTESIAN_POINT ( 'NONE',  ( 0.000000000000000000, 284.6994879831845537, 28.46994879831456515 ) ) ;
#13195=AXIS2_PLACEMENT_3D ( 'NONE', #12509, #3576, #7592 ) ;
#13201=DIRECTION ( 'NONE',  ( 0.000000000000000000, 0.9950371902099902632, -0.09950371902098713306 ) ) ;
#13203=ORIENTED_EDGE ( 'NONE', *, *, #8092, .T. ) ;
#13207=FACE_OUTER_BOUND ( 'NONE', #2428, .T. ) ;
#13302=CARTESIAN_POINT ( 'NONE',  ( 0.1218274893871210962, 285.8025109750047932, 37.43226525377778557 ) ) ;
#13303=EDGE_CURVE ( 'NONE', #15562, #12146, #3917, .T. ) ;
#13338=EDGE_LOOP ( 'NONE', ( #1153, #5014, #13181, #2747 ) ) ;
#13381=ORIENTED_EDGE ( 'NONE', *, *, #7050, .T. ) ;
#13383=CARTESIAN_POINT ( 'NONE',  ( -3.270000000000000462, 289.4632308570086821, 37.52989836422091230 ) ) ;
#13384=CARTESIAN_POINT ( 'NONE',  ( 0.7365999999999762737, 286.1765961517409664, 37.20123489369417058 ) ) ;
#13385=CYLINDRICAL_SURFACE ( 'NONE', #14290, 15.00000000000000000 ) ;
#13404=DIRECTION ( 'NONE',  ( 0.000000000000000000, 0.000000000000000000, 1.000000000000000000 ) ) ;
#13431=ORIENTED_EDGE ( 'NONE', *, *, #12966, .F. ) ;
#13471=FACE_OUTER_BOUND ( 'NONE', #1592, .T. ) ;
#13479=DIRECTION ( 'NONE',  ( -0.000000000000000000, 1.000000000000000000, -2.081668171172169499E-16 ) ) ;
#13523=CARTESIAN_POINT ( 'NONE',  ( -3.270000000000002238, 239.4632308570078294, 71.73739990498292229 ) ) ;
#13524=ORIENTED_EDGE ( 'NONE', *, *, #1108, .T. ) ;
#13544=CARTESIAN_POINT ( 'NONE',  ( 0.2121372864226510613, 189.4665531203498858, 37.56312099760641132 ) ) ;
#13549=FACE_OUTER_BOUND ( 'NONE', #13006, .T. ) ;
#13551=ORIENTED_EDGE ( 'NONE', *, *, #6211, .F. ) ;
#13557=CARTESIAN_POINT ( 'NONE',  ( 0.2120431089095113630, 289.4599079970928415, 37.56312696337874257 ) ) ;
#13560=AXIS2_PLACEMENT_3D ( 'NONE', #3460, #16591, #7383 ) ;
#13598=PRODUCT_DEFINITION_SHAPE ( 'NONE', 'NONE',  #10624 ) ;
#13610=DIRECTION ( 'NONE',  ( 4.930380657631322689E-32, 0.09950371902099953980, 0.9950371902099890420 ) ) ;
#13625=CARTESIAN_POINT ( 'NONE',  ( 0.7365999999999927050, 189.4632308570089094, 37.52989836422091940 ) ) ;
#13636=EDGE_CURVE ( 'NONE', #12302, #997, #15080, .T. ) ;
#13650=CARTESIAN_POINT ( 'NONE',  ( -3.197567832863594806, 192.4311383381408689, 37.56865621330425853 ) ) ;
#13687=ORIENTED_EDGE ( 'NONE', *, *, #3756, .F. ) ;
#13722=ORIENTED_EDGE ( 'NONE', *, *, #10007, .T. ) ;
#13729=CARTESIAN_POINT ( 'NONE',  ( -3.165718926336553274, 192.4396550164971700, 37.56780454546862558 ) ) ;
#13746=ORIENTED_EDGE ( 'NONE', *, *, #12341, .T. ) ;
#13760=CLOSED_SHELL ( 'NONE', ( #9712, #5936, #8824, #1354, #5065, #1738, #14568, #10927, #3820, #13965, #8981, #15886, #2771, #9676, #3539, #16933, #11077, #12031, #2994, #7511, #10410, #8770, #15706, #15573, #12611, #6311, #9005, #7087 ) ) ;
#13769=AXIS2_PLACEMENT_3D ( 'NONE', #2915, #8152, #13404 ) ;
#13771=VECTOR ( 'NONE', #10563, 1000.000000000000000 ) ;
#13777=CIRCLE ( 'NONE', #619, 15.00000000000000000 ) ;
#13789=DIRECTION ( 'NONE',  ( -0.000000000000000000, 0.09950371902100807464, -0.9950371902099882648 ) ) ;
#13849=ORIENTED_EDGE ( 'NONE', *, *, #4757, .F. ) ;
#13886=ORIENTED_EDGE ( 'NONE', *, *, #15669, .F. ) ;
#13890=CARTESIAN_POINT ( 'NONE',  ( 1.286622718088548112E-12, 260.4765148507136701, 287.1312267635912008 ) ) ;
#13893=CARTESIAN_POINT ( 'NONE',  ( -2.764312543576791015, 191.4687391198920920, 37.59778641568981072 ) ) ;
#13936=PLANE ( 'NONE',  #13560 ) ;
#13965=ADVANCED_FACE ( 'NONE', ( #13207 ), #6155, .F. ) ;
#13973=CARTESIAN_POINT ( 'NONE',  ( 1.231993379943791155E-12, 193.4898140233672450, 37.52989836422092651 ) ) ;
#13976=CARTESIAN_POINT ( 'NONE',  ( -3.269999999997899920, 192.9645375484312524, 37.54886512656518249 ) ) ;
#13979=FACE_OUTER_BOUND ( 'NONE', #2837, .T. ) ;
#13998=DIRECTION ( 'NONE',  ( 0.000000000000000000, -0.9950371902099846011, -0.09950371902104368504 ) ) ;
#14019=VERTEX_POINT ( 'NONE', #8734 ) ;
#14034=AXIS2_PLACEMENT_3D ( 'NONE', #11701, #11781, #16928 ) ;
#14084=CARTESIAN_POINT ( 'NONE',  ( 0.2121372864215120557, 289.4599085936700931, 37.56312099760677370 ) ) ;
#14090=VECTOR ( 'NONE', #16271, 1000.000000000000000 ) ;
#14095=LINE ( 'NONE', #15713, #1713 ) ;
#14124=FACE_OUTER_BOUND ( 'NONE', #12623, .T. ) ;
#14132=ORIENTED_EDGE ( 'NONE', *, *, #11385, .T. ) ;
#14151=VECTOR ( 'NONE', #393, 1000.000000000000114 ) ;
#14158=CARTESIAN_POINT ( 'NONE',  ( 56.72999999999999687, 183.8715257629570203, -18.38715257629581856 ) ) ;
#14166=ORIENTED_EDGE ( 'NONE', *, *, #2667, .F. ) ;
#14198=ORIENTED_EDGE ( 'NONE', *, *, #3756, .T. ) ;
#14201=B_SPLINE_CURVE_WITH_KNOTS ( 'NONE', 3,
 ( #16381, #7169, #12429, #4777, #6617, #13973 ),
 .UNSPECIFIED., .F., .F.,
 ( 4, 2, 4 ),
 ( 0.000000000000000000, 0.5000000000000000000, 1.000000000000000000 ),
 .UNSPECIFIED. ) ;
#14228=VECTOR ( 'NONE', #10383, 1000.000000000000114 ) ;
#14235=ORIENTED_EDGE ( 'NONE', *, *, #2434, .T. ) ;
#14280=CYLINDRICAL_SURFACE ( 'NONE', #14034, 4.006599999998781136 ) ;
#14284=DIRECTION ( 'NONE',  ( 2.920976200236518919E-15, -0.9950371902099892640, -0.09950371902099772181 ) ) ;
#14290=AXIS2_PLACEMENT_3D ( 'NONE', #6919, #418, #16203 ) ;
#14298=CARTESIAN_POINT ( 'NONE',  ( 0.7365999999999761627, 261.2094592450223445, 287.2045212030221251 ) ) ;
#14324=AXIS2_PLACEMENT_3D ( 'NONE', #1630, #5320, #9543 ) ;
#14340=AXIS2_PLACEMENT_3D ( 'NONE', #11321, #5748, #16224 ) ;
#14356=FACE_OUTER_BOUND ( 'NONE', #6777, .T. ) ;
#14392=EDGE_CURVE ( 'NONE', #9971, #1418, #15319, .T. ) ;
#14396=CARTESIAN_POINT ( 'NONE',  ( 56.73000000000001108, 239.4632308570078294, 56.73739990498292940 ) ) ;
#14417=VERTEX_POINT ( 'NONE', #3554 ) ;
#14418=LINE ( 'NONE', #11491, #12080 ) ;
#14447=EDGE_LOOP ( 'NONE', ( #9320, #7660, #5177, #10338 ) ) ;
#14455=EDGE_LOOP ( 'NONE', ( #9573, #4805 ) ) ;
#14461=LINE ( 'NONE', #2503, #1702 ) ;
#14462=FACE_OUTER_BOUND ( 'NONE', #7683, .T. ) ;
#14487=CARTESIAN_POINT ( 'NONE',  ( 56.73000000000001108, 239.4632308570078294, 86.73739990498292229 ) ) ;
#14497=CARTESIAN_POINT ( 'NONE',  ( 0.3042215205874465589, 286.0197353374350655, 37.35332311086187929 ) ) ;
#14520=LINE ( 'NONE', #1637, #9430 ) ;
#14521=CARTESIAN_POINT ( 'NONE',  ( 0.7366000000000268999, 217.7170024689957302, 287.2045212030222388 ) ) ;
#14568=ADVANCED_FACE ( 'NONE', ( #8067 ), #4304, .T. ) ;
#14572=CARTESIAN_POINT ( 'NONE',  ( -8.632284108936165032E-13, 289.4632308570086252, 37.52989836422091230 ) ) ;
#14577=CARTESIAN_POINT ( 'NONE',  ( -3.269999999998713491, 285.4366476906446906, 37.52989836422034386 ) ) ;
#14601=CARTESIAN_POINT ( 'NONE',  ( 1.250085104875786612E-12, 220.0768326692952996, 286.9685381829922903 ) ) ;
#14625=ORIENTED_EDGE ( 'NONE', *, *, #2667, .T. ) ;
#14635=CARTESIAN_POINT ( 'NONE',  ( 1.231978928595278688E-12, 193.4499468633042625, 37.13122676359134999 ) ) ;
#14672=CARTESIAN_POINT ( 'NONE',  ( 0.1739760006939537473, 285.8834916746054660, 37.40680846401821213 ) ) ;
#14731=CARTESIAN_POINT ( 'NONE',  ( -7.877607930108291241E-13, 264.4632308570089663, 287.5298983642207986 ) ) ;
#14748=LINE ( 'NONE', #14487, #4841 ) ;
#14757=CARTESIAN_POINT ( 'NONE',  ( -0.3121190734747821827, 289.3528227838037878, 37.58596727633977963 ) ) ;
#14758=CARTESIAN_POINT ( 'NONE',  ( 56.72999999999999687, 264.4632308570091368, 287.5298983642207986 ) ) ;
#14780=CARTESIAN_POINT ( 'NONE',  ( 1.286622718088548112E-12, 258.8496290447203023, 286.9685381829918924 ) ) ;
#14787=CARTESIAN_POINT ( 'NONE',  ( -3.270000000000002238, 239.4632308570078294, 71.73739990498292229 ) ) ;
#14834=VERTEX_POINT ( 'NONE', #5290 ) ;
#14850=SURFACE_STYLE_FILL_AREA ( #9614 ) ;
#14853=VECTOR ( 'NONE', #9062, 1000.000000000000227 ) ;
#14867=LINE ( 'NONE', #12291, #4829 ) ;
#14899=ORIENTED_EDGE ( 'NONE', *, *, #9099, .F. ) ;
#14908=CARTESIAN_POINT ( 'NONE',  ( -3.269999999998768114, 193.4898140233619017, 37.52989836422146652 ) ) ;
#14920=AXIS2_PLACEMENT_3D ( 'NONE', #1922, #7145, #8537 ) ;
#14935=CARTESIAN_POINT ( 'NONE',  ( 0.7366000000000039183, 192.7170024689980323, 37.20452120302198296 ) ) ;
#14955=ORIENTED_EDGE ( 'NONE', *, *, #10392, .T. ) ;
#14981=ORIENTED_EDGE ( 'NONE', *, *, #5174, .F. ) ;
#15016=CARTESIAN_POINT ( 'NONE',  ( -2.792885358475956092, 191.4523525084761673, 37.59942507683140178 ) ) ;
#15024=MECHANICAL_DESIGN_GEOMETRIC_PRESENTATION_REPRESENTATION('',(#222),#7601);
#15051=DIRECTION ( 'NONE',  ( -2.943801717315837579E-15, 0.9950371902099846011, 0.09950371902104368504 ) ) ;
#15053=ORIENTED_EDGE ( 'NONE', *, *, #14392, .T. ) ;
#15054=VERTEX_POINT ( 'NONE', #8480 ) ;
#15076=FACE_OUTER_BOUND ( 'NONE', #10312, .T. ) ;
#15077=VERTEX_POINT ( 'NONE', #12510 ) ;
#15080=CIRCLE ( 'NONE', #15889, 15.00000000000000000 ) ;
#15117=SHAPE_REPRESENTATION_RELATIONSHIP ( 'NONE' , 'NONE' ,  #135, #8557 ) ;
#15133=VECTOR ( 'NONE', #4996, 1000.000000000000114 ) ;
#15163=LINE ( 'NONE', #12263, #1519 ) ;
#15167=EDGE_CURVE ( 'NONE', #3191, #11441, #3577, .T. ) ;
#15179=ORIENTED_EDGE ( 'NONE', *, *, #1183, .F. ) ;
#15217=DIRECTION ( 'NONE',  ( 1.000000000000000000, 0.000000000000000000, 0.000000000000000000 ) ) ;
#15264=LINE ( 'NONE', #13890, #473 ) ;
#15313=ORIENTED_EDGE ( 'NONE', *, *, #8092, .F. ) ;
#15316=PRODUCT_DEFINITION_CONTEXT ( 'detailed design', #7630, 'design' ) ;
#15319=LINE ( 'NONE', #9105, #13771 ) ;
#15323=CARTESIAN_POINT ( 'NONE',  ( 1.286622718088548112E-12, 258.6869404641209940, 288.5954239889852602 ) ) ;
#15328=ORIENTED_EDGE ( 'NONE', *, *, #6870, .T. ) ;
#15427=ORIENTED_EDGE ( 'NONE', *, *, #6634, .F. ) ;
#15445=VECTOR ( 'NONE', #12029, 1000.000000000000000 ) ;
#15474=ORIENTED_EDGE ( 'NONE', *, *, #10766, .F. ) ;
#15496=CARTESIAN_POINT ( 'NONE',  ( -8.636442107178585067E-13, 290.3130897954760030, 29.03130897954724787 ) ) ;
#15535=CARTESIAN_POINT ( 'NONE',  ( 56.73000000000001108, 261.2094592450224582, 287.2045212030221251 ) ) ;
#15537=ORIENTED_EDGE ( 'NONE', *, *, #12250, .T. ) ;
#15562=VERTEX_POINT ( 'NONE', #13625 ) ;
#15567=EDGE_CURVE ( 'NONE', #8690, #14019, #5789, .T. ) ;
#15573=ADVANCED_FACE ( 'NONE', ( #814 ), #3227, .F. ) ;
#15599=CARTESIAN_POINT ( 'NONE',  ( 0.3042215205882442541, 192.9067263765842881, 37.35332311086163060 ) ) ;
#15601=PLANE ( 'NONE',  #9471 ) ;
#15622=CARTESIAN_POINT ( 'NONE',  ( 0.7365999999999761627, 286.2094592450219466, 37.20452120302238086 ) ) ;
#15627=ORIENTED_EDGE ( 'NONE', *, *, #3213, .T. ) ;
#15651=ORIENTED_EDGE ( 'NONE', *, *, #9959, .T. ) ;
#15661=VERTEX_POINT ( 'NONE', #11448 ) ;
#15669=EDGE_CURVE ( 'NONE', #4991, #14019, #2504, .T. ) ;
#15682=CARTESIAN_POINT ( 'NONE',  ( 1.250085104875786612E-12, 218.4499468633019603, 287.1312267635915987 ) ) ;
#15706=ADVANCED_FACE ( 'NONE', ( #14462 ), #4066, .F. ) ;
#15707=DIRECTION ( 'NONE',  ( 0.000000000000000000, 0.9950371902099903743, 0.09950371902098545385 ) ) ;
#15711=VECTOR ( 'NONE', #13610, 1000.000000000000227 ) ;
#15713=CARTESIAN_POINT ( 'NONE',  ( -3.269999999998768114, 193.4499468632989192, 37.13122676359189711 ) ) ;
#15714=DIRECTION ( 'NONE',  ( -8.929933532679207200E-16, 0.9950371902099895971, -0.09950371902099479360 ) ) ;
#15736=ORIENTED_EDGE ( 'NONE', *, *, #12571, .F. ) ;
#15757=LINE ( 'NONE', #13189, #11011 ) ;
#15768=LINE ( 'NONE', #14572, #9720 ) ;
#15769=FACE_OUTER_BOUND ( 'NONE', #11803, .T. ) ;
#15773=CARTESIAN_POINT ( 'NONE',  ( 0.1475654038900472698, 285.9036875807895512, 37.40882805463662208 ) ) ;
#15856=CARTESIAN_POINT ( 'NONE',  ( 0.6444877810225767556, 286.1732733541648486, 37.23446286945507921 ) ) ;
#15870=( LENGTH_UNIT ( ) NAMED_UNIT ( * ) SI_UNIT ( .MILLI., .METRE. ) );
#15884=CARTESIAN_POINT ( 'NONE',  ( 56.72999999999999687, 214.4632308570088810, 287.5298983642209123 ) ) ;
#15886=ADVANCED_FACE ( 'NONE', ( #8359 ), #462, .T. ) ;
#15889=AXIS2_PLACEMENT_3D ( 'NONE', #16220, #1626, #15962 ) ;
#15922=VERTEX_POINT ( 'NONE', #1832 ) ;
#15932=DIRECTION ( 'NONE',  ( -1.000000000000000000, -0.000000000000000000, -0.000000000000000000 ) ) ;
#15938=DIRECTION ( 'NONE',  ( -0.000000000000000000, 1.000000000000000000, -2.081668171172169499E-16 ) ) ;
#15940=CARTESIAN_POINT ( 'NONE',  ( -3.269999999999630536, 285.9619241655763631, 37.54886512656418063 ) ) ;
#15947=LINE ( 'NONE', #4026, #4193 ) ;
#15955=PLANE ( 'NONE',  #13769 ) ;
#15960=VECTOR ( 'NONE', #1877, 1000.000000000000000 ) ;
#15962=DIRECTION ( 'NONE',  ( 0.000000000000000000, 0.000000000000000000, 1.000000000000000000 ) ) ;
#15972=DIRECTION ( 'NONE',  ( -1.000000000000000000, -0.000000000000000000, 0.000000000000000000 ) ) ;
#15995=DIRECTION ( 'NONE',  ( 4.930380657631323236E-32, -0.09950371902099770793, 0.9950371902099891530 ) ) ;
#15999=CARTESIAN_POINT ( 'NONE',  ( 56.73000000000001108, 217.7170024689955596, 287.2045212030222388 ) ) ;
#16039=CARTESIAN_POINT ( 'NONE',  ( 0.09296894633892416326, 285.8190614525348110, 37.43392030153078309 ) ) ;
#16058=VECTOR ( 'NONE', #15938, 1000.000000000000000 ) ;
#16089=DIRECTION ( 'NONE',  ( 7.213771534993946619E-17, 0.09950371902098976984, 0.9950371902099900412 ) ) ;
#16146=DIRECTION ( 'NONE',  ( -1.000000000000000000, -0.000000000000000000, 0.000000000000000000 ) ) ;
#16149=ORIENTED_EDGE ( 'NONE', *, *, #6211, .T. ) ;
#16177=VERTEX_POINT ( 'NONE', #9279 ) ;
#16178=ORIENTED_EDGE ( 'NONE', *, *, #9317, .T. ) ;
#16203=DIRECTION ( 'NONE',  ( 0.000000000000000000, 0.000000000000000000, 1.000000000000000000 ) ) ;
#16211=EDGE_CURVE ( 'NONE', #12044, #12025, #1553, .T. ) ;
#16215=EDGE_CURVE ( 'NONE', #16177, #11437, #7783, .T. ) ;
#16220=CARTESIAN_POINT ( 'NONE',  ( 0.000000000000000000, 239.4632308570078294, 71.73739990498292229 ) ) ;
#16223=EDGE_CURVE ( 'NONE', #3191, #11237, #349, .T. ) ;
#16224=DIRECTION ( 'NONE',  ( 0.000000000000000000, 0.09950371902099770793, -0.9950371902099891530 ) ) ;
#16228=LINE ( 'NONE', #5486, #7217 ) ;
#16271=DIRECTION ( 'NONE',  ( -1.000000000000000000, 1.809417926841269906E-12, 1.809417926841437877E-13 ) ) ;
#16275=VECTOR ( 'NONE', #4808, 1000.000000000000114 ) ;
#16367=CARTESIAN_POINT ( 'NONE',  ( -3.270000000000000462, 220.1329686874181562, 287.5298983642209123 ) ) ;
#16381=CARTESIAN_POINT ( 'NONE',  ( 0.7366000000000088033, 192.7170024689980323, 37.20452120302199006 ) ) ;
#16384=CARTESIAN_POINT ( 'NONE',  ( 0.3656342590597776443, 192.8227990814932298, 37.32816098065109145 ) ) ;
#16390=DIRECTION ( 'NONE',  ( 7.213771534993946619E-17, 0.09950371902098976984, 0.9950371902099900412 ) ) ;
#16438=CARTESIAN_POINT ( 'NONE',  ( -2.467345170749142724, 191.0231794615330045, 37.60878752180606455 ) ) ;
#16468=VECTOR ( 'NONE', #12148, 1000.000000000000000 ) ;
#16510=ORIENTED_EDGE ( 'NONE', *, *, #13636, .T. ) ;
#16576=CARTESIAN_POINT ( 'NONE',  ( -1.281199806755509263, 288.9467639778929424, 37.61247111518800068 ) ) ;
#16582=PRODUCT_CONTEXT ( 'NONE', #4131, 'mechanical' ) ;
#16591=DIRECTION ( 'NONE',  ( -1.000000000000000000, -3.474153781073083121E-15, -3.474153781073041508E-16 ) ) ;
#16594=CARTESIAN_POINT ( 'NONE',  ( 56.73000000000000398, 189.4632308570087105, 37.52989836422094072 ) ) ;
#16629=ORIENTED_EDGE ( 'NONE', *, *, #15167, .T. ) ;
#16632=CARTESIAN_POINT ( 'NONE',  ( -1.745738565991610924, 190.2524942469967755, 37.61874632382036054 ) ) ;
#16653=ORIENTED_EDGE ( 'NONE', *, *, #1515, .T. ) ;
#16680=FACE_OUTER_BOUND ( 'NONE', #10214, .T. ) ;
#16726=DIRECTION ( 'NONE',  ( -1.000000000000000000, 0.000000000000000000, 6.123233995736766036E-17 ) ) ;
#16789=EDGE_LOOP ( 'NONE', ( #15313, #10116, #12947, #2866, #4863, #14235, #8108, #13687 ) ) ;
#16795=ORIENTED_EDGE ( 'NONE', *, *, #289, .T. ) ;
#16807=PLANE ( 'NONE',  #3301 ) ;
#16820=AXIS2_PLACEMENT_3D ( 'NONE', #2410, #11691, #12816 ) ;
#16908=VECTOR ( 'NONE', #15995, 1000.000000000000114 ) ;
#16909=DIRECTION ( 'NONE',  ( 7.213771534993946619E-17, 0.09950371902098976984, 0.9950371902099900412 ) ) ;
#16928=DIRECTION ( 'NONE',  ( -3.409610985204789889E-15, -0.9950371902099900412, 0.09950371902098964494 ) ) ;
#16933=ADVANCED_FACE ( 'NONE', ( #14124 ), #10259, .F. ) ;
ENDSEC;
END-ISO-10303-21;
